ISO-10303-21;
HEADER;
/* Generated by software containing ST-Developer
 * from STEP Tools, Inc. (www.steptools.com) 
 */

FILE_DESCRIPTION(
/* description */ ('Independent keyed three-contact power inlet for the IEC-connector des
ign category. Longer ground blade, retained contacts, wire termination
 holes and sealed bolted panel interface. Nominal custom interface; IE
C dimensional compatibility and electrical ratings are not assigned.'),

/* implementation_level */ '2;1');

FILE_NAME(
/* name */ 'Socket head cap screw M6x16.step',
/* time_stamp */ '2026-11-08T19:55:04-08:00',
/* author */ (''),
/* organization */ (''),
/* preprocessor_version */ 'ST-DEVELOPER v20.2',
/* originating_system */ 'Autodesk Translation Framework v15.17.0.0',
/* authorisation */ '');

FILE_SCHEMA (('AUTOMOTIVE_DESIGN { 1 0 10303 214 3 1 1 }'));
ENDSEC;

DATA;
#10=MECHANICAL_DESIGN_GEOMETRIC_PRESENTATION_REPRESENTATION('',(#116),#21880);
#80=CONICAL_SURFACE('',#6897,2.5,0.785398163397448);
#96=SHAPE_REPRESENTATION_RELATIONSHIP('SRR','None',#21932,#106);
#106=ADVANCED_BREP_SHAPE_REPRESENTATION('',(#126),#21877);
#116=STYLED_ITEM('',(#21986),#126);
#126=MANIFOLD_SOLID_BREP('Body1',#6388);
#139=B_SPLINE_SURFACE_WITH_KNOTS('',3,3,((#19619,#19620,#19621,#19622,#19623,
#19624,#19625,#19626,#19627,#19628,#19629,#19630,#19631,#19632,#19633,#19634,
#19635,#19636,#19637,#19638,#19639,#19640,#19641,#19642,#19643,#19644,#19645,
#19646,#19647,#19648,#19649,#19650,#19651,#19652,#19653,#19654,#19655,#19656,
#19657,#19658,#19659,#19660,#19661,#19662,#19663,#19664,#19665,#19666,#19667,
#19668,#19669,#19670,#19671,#19672,#19673,#19674,#19675,#19676,#19677,#19678,
#19679,#19680,#19681,#19682,#19683,#19684,#19685,#19686,#19687,#19688,#19689,
#19690,#19691,#19692,#19693,#19694,#19695,#19696,#19697,#19698,#19699,#19700,
#19701,#19702,#19703,#19704,#19705,#19706,#19707,#19708,#19709,#19710,#19711,
#19712,#19713,#19714,#19715,#19716,#19717,#19718,#19719,#19720),(#19721,
#19722,#19723,#19724,#19725,#19726,#19727,#19728,#19729,#19730,#19731,#19732,
#19733,#19734,#19735,#19736,#19737,#19738,#19739,#19740,#19741,#19742,#19743,
#19744,#19745,#19746,#19747,#19748,#19749,#19750,#19751,#19752,#19753,#19754,
#19755,#19756,#19757,#19758,#19759,#19760,#19761,#19762,#19763,#19764,#19765,
#19766,#19767,#19768,#19769,#19770,#19771,#19772,#19773,#19774,#19775,#19776,
#19777,#19778,#19779,#19780,#19781,#19782,#19783,#19784,#19785,#19786,#19787,
#19788,#19789,#19790,#19791,#19792,#19793,#19794,#19795,#19796,#19797,#19798,
#19799,#19800,#19801,#19802,#19803,#19804,#19805,#19806,#19807,#19808,#19809,
#19810,#19811,#19812,#19813,#19814,#19815,#19816,#19817,#19818,#19819,#19820,
#19821,#19822),(#19823,#19824,#19825,#19826,#19827,#19828,#19829,#19830,
#19831,#19832,#19833,#19834,#19835,#19836,#19837,#19838,#19839,#19840,#19841,
#19842,#19843,#19844,#19845,#19846,#19847,#19848,#19849,#19850,#19851,#19852,
#19853,#19854,#19855,#19856,#19857,#19858,#19859,#19860,#19861,#19862,#19863,
#19864,#19865,#19866,#19867,#19868,#19869,#19870,#19871,#19872,#19873,#19874,
#19875,#19876,#19877,#19878,#19879,#19880,#19881,#19882,#19883,#19884,#19885,
#19886,#19887,#19888,#19889,#19890,#19891,#19892,#19893,#19894,#19895,#19896,
#19897,#19898,#19899,#19900,#19901,#19902,#19903,#19904,#19905,#19906,#19907,
#19908,#19909,#19910,#19911,#19912,#19913,#19914,#19915,#19916,#19917,#19918,
#19919,#19920,#19921,#19922,#19923,#19924),(#19925,#19926,#19927,#19928,
#19929,#19930,#19931,#19932,#19933,#19934,#19935,#19936,#19937,#19938,#19939,
#19940,#19941,#19942,#19943,#19944,#19945,#19946,#19947,#19948,#19949,#19950,
#19951,#19952,#19953,#19954,#19955,#19956,#19957,#19958,#19959,#19960,#19961,
#19962,#19963,#19964,#19965,#19966,#19967,#19968,#19969,#19970,#19971,#19972,
#19973,#19974,#19975,#19976,#19977,#19978,#19979,#19980,#19981,#19982,#19983,
#19984,#19985,#19986,#19987,#19988,#19989,#19990,#19991,#19992,#19993,#19994,
#19995,#19996,#19997,#19998,#19999,#20000,#20001,#20002,#20003,#20004,#20005,
#20006,#20007,#20008,#20009,#20010,#20011,#20012,#20013,#20014,#20015,#20016,
#20017,#20018,#20019,#20020,#20021,#20022,#20023,#20024,#20025,#20026)),
 .UNSPECIFIED.,.F.,.F.,.F.,(4,4),(4,1,1,1,1,1,1,1,1,1,1,1,1,1,1,1,1,1,1,
1,1,1,1,1,1,1,1,1,1,1,1,1,1,1,1,1,1,1,1,1,1,1,1,1,1,1,1,1,1,1,1,1,1,1,1,
1,1,1,1,1,1,1,1,1,1,1,1,1,1,1,1,1,1,1,1,1,1,1,1,1,1,1,1,1,1,1,1,1,1,1,1,
1,1,1,1,1,1,1,1,4),(0.,0.0658467982010768),(11.6150328478182,12.6069034617266,
13.598774075635,14.5906446895433,15.5825153034517,16.5743859173601,17.5662565312685,
18.5581271451769,19.5499977590852,20.5418683729936,21.533738986902,22.5256096008104,
23.5174802147187,24.5093508286271,25.5012214425355,26.4930920564439,27.4849626703523,
28.4768332842606,29.468703898169,30.4605745120774,31.4524451259858,32.4443157398941,
33.4361863538025,34.4280569677109,35.4199275816193,36.4117981955277,37.403668809436,
38.3955394233444,39.3874100372528,40.3792806511612,41.3711512650695,42.3630218789779,
43.3548924928863,44.3467631067947,45.3386337207031,46.3305043346114,47.3223749485198,
48.3142455624282,49.3061161763366,50.2979867902449,51.2898574041533,52.2817280180617,
53.2735986319701,54.2654692458785,55.2573398597868,56.2492104736952,57.2410810876036,
58.232951701512,59.2248223154203,60.2166929293287,61.2085635432371,62.2004341571455,
63.1923047710539,64.1841753849622,65.1760459988706,66.167916612779,67.1597872266874,
68.1516578405957,69.1435284545041,70.1353990684125,71.1272696823209,72.1191402962293,
73.1110109101376,74.102881524046,75.0947521379544,76.0866227518628,77.0784933657711,
78.0703639796795,79.0622345935879,80.0541052074963,81.0459758214047,82.037846435313,
83.0297170492214,84.0215876631298,85.0134582770382,86.0053288909465,86.9971995048549,
87.9890701187633,88.9809407326717,89.9728113465801,90.9646819604884,91.9565525743968,
92.9484231883052,93.9402938022136,94.9321644161219,95.9240350300303,96.9159056439387,
97.9077762578471,98.8996468717555,99.8915174856638,100.883388099572,101.875258713481,
102.867129327389,103.858999941297,104.850870555206,105.842741169114,106.834611783022,
107.826482396931,108.818353010839,109.810223624748),.UNSPECIFIED.);
#140=B_SPLINE_SURFACE_WITH_KNOTS('',3,3,((#20155,#20156,#20157,#20158,#20159,
#20160,#20161,#20162,#20163,#20164,#20165,#20166,#20167,#20168,#20169,#20170,
#20171,#20172,#20173,#20174,#20175,#20176,#20177,#20178,#20179,#20180,#20181,
#20182,#20183,#20184,#20185,#20186,#20187,#20188,#20189,#20190,#20191,#20192,
#20193,#20194,#20195,#20196,#20197,#20198,#20199,#20200,#20201,#20202,#20203,
#20204,#20205,#20206,#20207,#20208,#20209,#20210,#20211,#20212,#20213,#20214,
#20215,#20216,#20217,#20218,#20219,#20220,#20221,#20222,#20223,#20224,#20225,
#20226,#20227,#20228,#20229,#20230,#20231,#20232,#20233,#20234,#20235,#20236,
#20237,#20238,#20239,#20240,#20241,#20242,#20243,#20244,#20245,#20246,#20247,
#20248,#20249,#20250,#20251,#20252,#20253,#20254,#20255,#20256,#20257,#20258),
(#20259,#20260,#20261,#20262,#20263,#20264,#20265,#20266,#20267,#20268,
#20269,#20270,#20271,#20272,#20273,#20274,#20275,#20276,#20277,#20278,#20279,
#20280,#20281,#20282,#20283,#20284,#20285,#20286,#20287,#20288,#20289,#20290,
#20291,#20292,#20293,#20294,#20295,#20296,#20297,#20298,#20299,#20300,#20301,
#20302,#20303,#20304,#20305,#20306,#20307,#20308,#20309,#20310,#20311,#20312,
#20313,#20314,#20315,#20316,#20317,#20318,#20319,#20320,#20321,#20322,#20323,
#20324,#20325,#20326,#20327,#20328,#20329,#20330,#20331,#20332,#20333,#20334,
#20335,#20336,#20337,#20338,#20339,#20340,#20341,#20342,#20343,#20344,#20345,
#20346,#20347,#20348,#20349,#20350,#20351,#20352,#20353,#20354,#20355,#20356,
#20357,#20358,#20359,#20360,#20361,#20362),(#20363,#20364,#20365,#20366,
#20367,#20368,#20369,#20370,#20371,#20372,#20373,#20374,#20375,#20376,#20377,
#20378,#20379,#20380,#20381,#20382,#20383,#20384,#20385,#20386,#20387,#20388,
#20389,#20390,#20391,#20392,#20393,#20394,#20395,#20396,#20397,#20398,#20399,
#20400,#20401,#20402,#20403,#20404,#20405,#20406,#20407,#20408,#20409,#20410,
#20411,#20412,#20413,#20414,#20415,#20416,#20417,#20418,#20419,#20420,#20421,
#20422,#20423,#20424,#20425,#20426,#20427,#20428,#20429,#20430,#20431,#20432,
#20433,#20434,#20435,#20436,#20437,#20438,#20439,#20440,#20441,#20442,#20443,
#20444,#20445,#20446,#20447,#20448,#20449,#20450,#20451,#20452,#20453,#20454,
#20455,#20456,#20457,#20458,#20459,#20460,#20461,#20462,#20463,#20464,#20465,
#20466),(#20467,#20468,#20469,#20470,#20471,#20472,#20473,#20474,#20475,
#20476,#20477,#20478,#20479,#20480,#20481,#20482,#20483,#20484,#20485,#20486,
#20487,#20488,#20489,#20490,#20491,#20492,#20493,#20494,#20495,#20496,#20497,
#20498,#20499,#20500,#20501,#20502,#20503,#20504,#20505,#20506,#20507,#20508,
#20509,#20510,#20511,#20512,#20513,#20514,#20515,#20516,#20517,#20518,#20519,
#20520,#20521,#20522,#20523,#20524,#20525,#20526,#20527,#20528,#20529,#20530,
#20531,#20532,#20533,#20534,#20535,#20536,#20537,#20538,#20539,#20540,#20541,
#20542,#20543,#20544,#20545,#20546,#20547,#20548,#20549,#20550,#20551,#20552,
#20553,#20554,#20555,#20556,#20557,#20558,#20559,#20560,#20561,#20562,#20563,
#20564,#20565,#20566,#20567,#20568,#20569,#20570)),.UNSPECIFIED.,.F.,.F.,
 .F.,(4,4),(4,1,1,1,1,1,1,1,1,1,1,1,1,1,1,1,1,1,1,1,1,1,1,1,1,1,1,1,1,1,
1,1,1,1,1,1,1,1,1,1,1,1,1,1,1,1,1,1,1,1,1,1,1,1,1,1,1,1,1,1,1,1,1,1,1,1,
1,1,1,1,1,1,1,1,1,1,1,1,1,1,1,1,1,1,1,1,1,1,1,1,1,1,1,1,1,1,1,1,1,1,1,4),
(0.,0.0658467982010768),(8.30747755240101,9.30018873014199,10.292899907883,
11.2856110856239,12.2783222633649,13.2710334411059,14.2637446188469,15.2564557965878,
16.2491669743288,17.2418781520698,18.2345893298108,19.2273005075518,20.2200116852927,
21.2127228630337,22.2054340407747,23.1981452185157,24.1908563962566,25.1835675739976,
26.1762787517386,27.1689899294796,28.1617011072206,29.1544122849615,30.1471234627025,
31.1398346404435,32.1325458181845,33.1252569959254,34.1179681736664,35.1106793514074,
36.1033905291484,37.0961017068893,38.0888128846303,39.0815240623713,40.0742352401123,
41.0669464178533,42.0596575955942,43.0523687733352,44.0450799510762,45.0377911288172,
46.0305023065581,47.0232134842991,48.0159246620401,49.0086358397811,50.001347017522,
50.994058195263,51.986769373004,52.979480550745,53.972191728486,54.9649029062269,
55.9576140839679,56.9503252617089,57.9430364394499,58.9357476171908,59.9284587949318,
60.9211699726728,61.9138811504138,62.9065923281547,63.8993035058957,64.8920146836367,
65.8847258613777,66.8774370391187,67.8701482168596,68.8628593946006,69.8555705723416,
70.8482817500825,71.8409929278235,72.8337041055645,73.8264152833055,74.8191264610465,
75.8118376387874,76.8045488165284,77.7972599942694,78.7899711720104,79.7826823497514,
80.7753935274923,81.7681047052333,82.7608158829743,83.7535270607153,84.7462382384562,
85.7389494161972,86.7316605939382,87.7243717716792,88.7170829494201,89.7097941271611,
90.7025053049021,91.6952164826431,92.687927660384,93.680638838125,94.673350015866,
95.666061193607,96.658772371348,97.6514835490889,98.6441947268299,99.6369059045709,
100.629617082312,101.622328260053,102.615039437794,103.607750615535,104.600461793276,
105.593172971017,106.585884148758,107.578595326499,108.57130650424),
 .UNSPECIFIED.);
#191=FACE_BOUND('',#1032,.T.);
#192=FACE_BOUND('',#1035,.T.);
#293=PLANE('',#6903);
#294=PLANE('',#6904);
#295=PLANE('',#6905);
#296=PLANE('',#6906);
#297=PLANE('',#6907);
#298=PLANE('',#6908);
#299=PLANE('',#6909);
#300=PLANE('',#6910);
#301=PLANE('',#6914);
#302=PLANE('',#6915);
#597=FACE_OUTER_BOUND('',#989,.T.);
#598=FACE_OUTER_BOUND('',#990,.T.);
#599=FACE_OUTER_BOUND('',#991,.T.);
#600=FACE_OUTER_BOUND('',#992,.T.);
#601=FACE_OUTER_BOUND('',#993,.T.);
#602=FACE_OUTER_BOUND('',#994,.T.);
#603=FACE_OUTER_BOUND('',#995,.T.);
#604=FACE_OUTER_BOUND('',#996,.T.);
#605=FACE_OUTER_BOUND('',#997,.T.);
#606=FACE_OUTER_BOUND('',#998,.T.);
#607=FACE_OUTER_BOUND('',#999,.T.);
#608=FACE_OUTER_BOUND('',#1000,.T.);
#609=FACE_OUTER_BOUND('',#1001,.T.);
#610=FACE_OUTER_BOUND('',#1002,.T.);
#611=FACE_OUTER_BOUND('',#1003,.T.);
#612=FACE_OUTER_BOUND('',#1004,.T.);
#613=FACE_OUTER_BOUND('',#1005,.T.);
#614=FACE_OUTER_BOUND('',#1006,.T.);
#615=FACE_OUTER_BOUND('',#1007,.T.);
#616=FACE_OUTER_BOUND('',#1008,.T.);
#617=FACE_OUTER_BOUND('',#1009,.T.);
#618=FACE_OUTER_BOUND('',#1010,.T.);
#619=FACE_OUTER_BOUND('',#1011,.T.);
#620=FACE_OUTER_BOUND('',#1012,.T.);
#621=FACE_OUTER_BOUND('',#1013,.T.);
#622=FACE_OUTER_BOUND('',#1014,.T.);
#623=FACE_OUTER_BOUND('',#1015,.T.);
#624=FACE_OUTER_BOUND('',#1016,.T.);
#625=FACE_OUTER_BOUND('',#1017,.T.);
#626=FACE_OUTER_BOUND('',#1018,.T.);
#627=FACE_OUTER_BOUND('',#1019,.T.);
#628=FACE_OUTER_BOUND('',#1020,.T.);
#629=FACE_OUTER_BOUND('',#1021,.T.);
#630=FACE_OUTER_BOUND('',#1022,.T.);
#631=FACE_OUTER_BOUND('',#1023,.T.);
#632=FACE_OUTER_BOUND('',#1024,.T.);
#633=FACE_OUTER_BOUND('',#1025,.T.);
#634=FACE_OUTER_BOUND('',#1026,.T.);
#635=FACE_OUTER_BOUND('',#1027,.T.);
#636=FACE_OUTER_BOUND('',#1028,.T.);
#637=FACE_OUTER_BOUND('',#1029,.T.);
#638=FACE_OUTER_BOUND('',#1030,.T.);
#639=FACE_OUTER_BOUND('',#1031,.T.);
#640=FACE_OUTER_BOUND('',#1033,.T.);
#641=FACE_OUTER_BOUND('',#1034,.T.);
#642=FACE_OUTER_BOUND('',#1036,.T.);
#989=EDGE_LOOP('',(#5447,#5448,#5449,#5450));
#990=EDGE_LOOP('',(#5451,#5452,#5453,#5454));
#991=EDGE_LOOP('',(#5455,#5456,#5457,#5458));
#992=EDGE_LOOP('',(#5459,#5460,#5461,#5462));
#993=EDGE_LOOP('',(#5463,#5464,#5465,#5466));
#994=EDGE_LOOP('',(#5467,#5468,#5469,#5470));
#995=EDGE_LOOP('',(#5471,#5472,#5473,#5474));
#996=EDGE_LOOP('',(#5475,#5476,#5477,#5478));
#997=EDGE_LOOP('',(#5479,#5480,#5481,#5482));
#998=EDGE_LOOP('',(#5483,#5484,#5485,#5486));
#999=EDGE_LOOP('',(#5487,#5488,#5489,#5490));
#1000=EDGE_LOOP('',(#5491,#5492,#5493,#5494));
#1001=EDGE_LOOP('',(#5495,#5496,#5497,#5498));
#1002=EDGE_LOOP('',(#5499,#5500,#5501,#5502));
#1003=EDGE_LOOP('',(#5503,#5504,#5505,#5506));
#1004=EDGE_LOOP('',(#5507,#5508,#5509,#5510));
#1005=EDGE_LOOP('',(#5511,#5512,#5513,#5514));
#1006=EDGE_LOOP('',(#5515,#5516,#5517,#5518));
#1007=EDGE_LOOP('',(#5519,#5520,#5521,#5522));
#1008=EDGE_LOOP('',(#5523,#5524,#5525,#5526));
#1009=EDGE_LOOP('',(#5527,#5528,#5529,#5530));
#1010=EDGE_LOOP('',(#5531,#5532,#5533,#5534));
#1011=EDGE_LOOP('',(#5535,#5536,#5537,#5538));
#1012=EDGE_LOOP('',(#5539,#5540,#5541,#5542));
#1013=EDGE_LOOP('',(#5543,#5544,#5545,#5546));
#1014=EDGE_LOOP('',(#5547,#5548,#5549,#5550));
#1015=EDGE_LOOP('',(#5551,#5552,#5553,#5554));
#1016=EDGE_LOOP('',(#5555,#5556,#5557,#5558));
#1017=EDGE_LOOP('',(#5559,#5560,#5561,#5562));
#1018=EDGE_LOOP('',(#5563,#5564,#5565,#5566));
#1019=EDGE_LOOP('',(#5567,#5568,#5569,#5570,#5571,#5572,#5573,#5574));
#1020=EDGE_LOOP('',(#5575,#5576,#5577,#5578,#5579,#5580,#5581,#5582,#5583,
#5584,#5585,#5586,#5587,#5588,#5589,#5590,#5591,#5592,#5593,#5594,#5595,
#5596,#5597,#5598,#5599,#5600,#5601,#5602,#5603,#5604,#5605,#5606,#5607,
#5608));
#1021=EDGE_LOOP('',(#5609,#5610,#5611,#5612));
#1022=EDGE_LOOP('',(#5613,#5614,#5615,#5616,#5617,#5618,#5619,#5620,#5621,
#5622,#5623,#5624,#5625,#5626,#5627,#5628,#5629,#5630,#5631,#5632,#5633,
#5634,#5635,#5636,#5637,#5638,#5639,#5640,#5641,#5642,#5643,#5644,#5645,
#5646,#5647));
#1023=EDGE_LOOP('',(#5648,#5649,#5650,#5651));
#1024=EDGE_LOOP('',(#5652,#5653,#5654,#5655));
#1025=EDGE_LOOP('',(#5656,#5657,#5658,#5659));
#1026=EDGE_LOOP('',(#5660,#5661,#5662,#5663));
#1027=EDGE_LOOP('',(#5664,#5665,#5666,#5667));
#1028=EDGE_LOOP('',(#5668,#5669,#5670,#5671));
#1029=EDGE_LOOP('',(#5672,#5673,#5674,#5675));
#1030=EDGE_LOOP('',(#5676,#5677,#5678,#5679,#5680,#5681));
#1031=EDGE_LOOP('',(#5682));
#1032=EDGE_LOOP('',(#5683,#5684,#5685,#5686));
#1033=EDGE_LOOP('',(#5687,#5688,#5689,#5690));
#1034=EDGE_LOOP('',(#5691));
#1035=EDGE_LOOP('',(#5692,#5693,#5694,#5695,#5696,#5697));
#1036=EDGE_LOOP('',(#5698));
#1147=CIRCLE('',#6866,2.942);
#1148=CIRCLE('',#6882,2.37175);
#1149=CIRCLE('',#6898,2.942);
#1150=CIRCLE('',#6899,2.);
#1151=CIRCLE('',#6901,2.37175);
#1152=CIRCLE('',#6911,5.);
#1153=CIRCLE('',#6913,5.);
#1432=B_SPLINE_CURVE_WITH_KNOTS('',3,(#18211,#18212,#18213,#18214,#18215,
#18216,#18217,#18218,#18219,#18220),.UNSPECIFIED.,.F.,.F.,(4,3,3,4),(-4.09293042013066,
-3.96748245563351,-2.97561184172513,-2.06863817490915),.UNSPECIFIED.);
#1433=B_SPLINE_CURVE_WITH_KNOTS('',3,(#18223,#18224,#18225,#18226,#18227,
#18228,#18229),.UNSPECIFIED.,.F.,.F.,(4,3,4),(0.,0.992711177740983,1.1173004083682),
 .UNSPECIFIED.);
#1434=B_SPLINE_CURVE_WITH_KNOTS('',3,(#18234,#18235,#18236,#18237,#18238,
#18239,#18240,#18241,#18242,#18243,#18244,#18245,#18246,#18247,#18248,#18249,
#18250,#18251,#18252,#18253,#18254,#18255),.UNSPECIFIED.,.F.,.F.,(4,3,3,
3,3,3,3,4),(-10.3761157273102,-9.91870613908378,-8.9268355251754,-7.93496491126702,
-6.94309429735864,-5.95122368345026,-4.95935306954189,-4.09293042013066),
 .UNSPECIFIED.);
#1435=B_SPLINE_CURVE_WITH_KNOTS('',3,(#18256,#18257,#18258,#18259,#18260,
#18261,#18262,#18263,#18264,#18265,#18266,#18267,#18268,#18269,#18270,#18271,
#18272,#18273,#18274,#18275,#18276,#18277),.UNSPECIFIED.,.F.,.F.,(4,3,3,
3,3,3,3,4),(1.1173004083682,1.98542235548196,2.97813353322293,3.97084471096391,
4.96355588870488,5.95626706644586,6.94897824418683,7.40048571554779),
 .UNSPECIFIED.);
#1436=B_SPLINE_CURVE_WITH_KNOTS('',3,(#18282,#18283,#18284,#18285,#18286,
#18287,#18288,#18289,#18290,#18291,#18292,#18293,#18294,#18295,#18296,#18297,
#18298,#18299,#18300,#18301,#18302,#18303),.UNSPECIFIED.,.F.,.F.,(4,3,3,
3,3,3,3,4),(-16.6593010344898,-15.869929822534,-14.8780592086257,-13.8861885947173,
-12.8943179808089,-11.9024473669005,-10.9105767529922,-10.3761157273102),
 .UNSPECIFIED.);
#1437=B_SPLINE_CURVE_WITH_KNOTS('',3,(#18304,#18305,#18306,#18307,#18308,
#18309,#18310,#18311,#18312,#18313,#18314,#18315,#18316,#18317,#18318,#18319,
#18320,#18321,#18322,#18323,#18324,#18325),.UNSPECIFIED.,.F.,.F.,(4,3,3,
3,3,3,3,4),(7.40048571554779,7.94168942192781,8.93440059966879,9.92711177740977,
10.9198229551507,11.9125341328917,12.9052453106327,13.6836710227274),
 .UNSPECIFIED.);
#1438=B_SPLINE_CURVE_WITH_KNOTS('',3,(#18330,#18331,#18332,#18333,#18334,
#18335,#18336,#18337,#18338,#18339,#18340,#18341,#18342,#18343,#18344,#18345,
#18346,#18347,#18348,#18349,#18350,#18351,#18352,#18353,#18354),
 .UNSPECIFIED.,.F.,.F.,(4,3,3,3,3,3,3,3,4),(-22.9424863416694,-22.8130241198927,
-21.8211535059843,-20.8292828920759,-19.8374122781676,-18.8455416642592,
-17.8536710503508,-16.8618004364424,-16.6593010344898),.UNSPECIFIED.);
#1439=B_SPLINE_CURVE_WITH_KNOTS('',3,(#18355,#18356,#18357,#18358,#18359,
#18360,#18361,#18362,#18363,#18364,#18365,#18366,#18367,#18368,#18369,#18370,
#18371,#18372,#18373,#18374,#18375,#18376,#18377,#18378,#18379),
 .UNSPECIFIED.,.F.,.F.,(4,3,3,3,3,3,3,3,4),(13.6836710227274,13.8979564883737,
14.8906676661147,15.8833788438556,16.8760900215966,17.8688011993376,18.8615123770786,
19.8542235548195,19.966856329907),.UNSPECIFIED.);
#1440=B_SPLINE_CURVE_WITH_KNOTS('',3,(#18384,#18385,#18386,#18387,#18388,
#18389,#18390,#18391,#18392,#18393,#18394,#18395,#18396,#18397,#18398,#18399,
#18400,#18401,#18402,#18403,#18404,#18405),.UNSPECIFIED.,.F.,.F.,(4,3,3,
3,3,3,3,4),(-29.225671648849,-28.764247803343,-27.7723771894346,-26.7805065755262,
-25.7886359616178,-24.7967653477094,-23.8048947338011,-22.9424863416694),
 .UNSPECIFIED.);
#1441=B_SPLINE_CURVE_WITH_KNOTS('',3,(#18406,#18407,#18408,#18409,#18410,
#18411,#18412,#18413,#18414,#18415,#18416,#18417,#18418,#18419,#18420,#18421,
#18422,#18423,#18424,#18425,#18426,#18427),.UNSPECIFIED.,.F.,.F.,(4,3,3,
3,3,3,3,4),(19.966856329907,20.8469347325605,21.8396459103015,22.8323570880425,
23.8250682657834,24.8177794435244,25.8104906212654,26.2500416370865),
 .UNSPECIFIED.);
#1442=B_SPLINE_CURVE_WITH_KNOTS('',3,(#18432,#18433,#18434,#18435,#18436,
#18437,#18438,#18439,#18440,#18441,#18442,#18443,#18444,#18445,#18446,#18447,
#18448,#18449,#18450,#18451,#18452,#18453),.UNSPECIFIED.,.F.,.F.,(4,3,3,
3,3,3,3,4),(-35.5088569560286,-34.7154714867932,-33.7236008728848,-32.7317302589765,
-31.7398596450681,-30.7479890311597,-29.7561184172513,-29.225671648849),
 .UNSPECIFIED.);
#1443=B_SPLINE_CURVE_WITH_KNOTS('',3,(#18454,#18455,#18456,#18457,#18458,
#18459,#18460,#18461,#18462,#18463,#18464,#18465,#18466,#18467,#18468,#18469,
#18470,#18471,#18472,#18473,#18474,#18475),.UNSPECIFIED.,.F.,.F.,(4,3,3,
3,3,3,3,4),(26.2500416370865,26.8032017990064,27.7959129767474,28.7886241544883,
29.7813353322293,30.7740465099703,31.7667576877113,32.5332269442661),
 .UNSPECIFIED.);
#1444=B_SPLINE_CURVE_WITH_KNOTS('',3,(#18480,#18481,#18482,#18483,#18484,
#18485,#18486,#18487,#18488,#18489,#18490,#18491,#18492,#18493,#18494,#18495,
#18496,#18497,#18498,#18499,#18500,#18501,#18502,#18503,#18504),
 .UNSPECIFIED.,.F.,.F.,(4,3,3,3,3,3,3,3,4),(-41.7920422632082,-41.6585657841519,
-40.6666951702435,-39.6748245563351,-38.6829539424267,-37.6910833285184,
-36.69921271461,-35.7073421007016,-35.5088569560286),.UNSPECIFIED.);
#1445=B_SPLINE_CURVE_WITH_KNOTS('',3,(#18505,#18506,#18507,#18508,#18509,
#18510,#18511,#18512,#18513,#18514,#18515,#18516,#18517,#18518,#18519,#18520,
#18521,#18522,#18523,#18524,#18525,#18526,#18527,#18528,#18529),
 .UNSPECIFIED.,.F.,.F.,(4,3,3,3,3,3,3,3,4),(32.5332269442661,32.7594688654522,
33.7521800431932,34.7448912209342,35.7376023986752,36.7303135764161,37.7230247541571,
38.7157359318981,38.8164122514457),.UNSPECIFIED.);
#1446=B_SPLINE_CURVE_WITH_KNOTS('',3,(#18534,#18535,#18536,#18537,#18538,
#18539,#18540,#18541,#18542,#18543,#18544,#18545,#18546,#18547,#18548,#18549,
#18550,#18551,#18552,#18553,#18554,#18555),.UNSPECIFIED.,.F.,.F.,(4,3,3,
3,3,3,3,4),(-48.0752275703878,-47.6097894676021,-46.6179188536938,-45.6260482397854,
-44.634177625877,-43.6423070119686,-42.6504363980602,-41.7920422632082),
 .UNSPECIFIED.);
#1447=B_SPLINE_CURVE_WITH_KNOTS('',3,(#18556,#18557,#18558,#18559,#18560,
#18561,#18562,#18563,#18564,#18565,#18566,#18567,#18568,#18569,#18570,#18571,
#18572,#18573,#18574,#18575,#18576,#18577),.UNSPECIFIED.,.F.,.F.,(4,3,3,
3,3,3,3,4),(38.8164122514457,39.7084471096391,40.7011582873801,41.693869465121,
42.686580642862,43.679291820603,44.672002998344,45.0995975586253),
 .UNSPECIFIED.);
#1448=B_SPLINE_CURVE_WITH_KNOTS('',3,(#18582,#18583,#18584,#18585,#18586,
#18587,#18588,#18589,#18590,#18591,#18592,#18593,#18594,#18595,#18596,#18597,
#18598,#18599,#18600,#18601,#18602,#18603),.UNSPECIFIED.,.F.,.F.,(4,3,3,
3,3,3,3,4),(-54.3584128775674,-53.5610131510524,-52.569142537144,-51.5772719232356,
-50.5854013093273,-49.5935306954189,-48.6016600815105,-48.0752275703878),
 .UNSPECIFIED.);
#1449=B_SPLINE_CURVE_WITH_KNOTS('',3,(#18604,#18605,#18606,#18607,#18608,
#18609,#18610,#18611,#18612,#18613,#18614,#18615,#18616,#18617,#18618,#18619,
#18620,#18621,#18622,#18623,#18624,#18625),.UNSPECIFIED.,.F.,.F.,(4,3,3,
3,3,3,3,4),(45.0995975586253,45.6647141760849,46.6574253538259,47.6501365315669,
48.6428477093079,49.6355588870488,50.6282700647898,51.3827828658049),
 .UNSPECIFIED.);
#1450=B_SPLINE_CURVE_WITH_KNOTS('',3,(#18630,#18631,#18632,#18633,#18634,
#18635,#18636,#18637,#18638,#18639,#18640,#18641,#18642,#18643,#18644,#18645,
#18646,#18647,#18648,#18649,#18650,#18651,#18652,#18653,#18654),
 .UNSPECIFIED.,.F.,.F.,(4,3,3,3,3,3,3,3,4),(-60.641598184747,-60.5041074484111,
-59.5122368345027,-58.5203662205943,-57.5284956066859,-56.5366249927775,
-55.5447543788692,-54.5528837649608,-54.3584128775674),.UNSPECIFIED.);
#1451=B_SPLINE_CURVE_WITH_KNOTS('',3,(#18655,#18656,#18657,#18658,#18659,
#18660,#18661,#18662,#18663,#18664,#18665,#18666,#18667,#18668,#18669,#18670,
#18671,#18672,#18673,#18674,#18675,#18676,#18677,#18678,#18679),
 .UNSPECIFIED.,.F.,.F.,(4,3,3,3,3,3,3,3,4),(51.3827828658049,51.6209812425308,
52.6136924202718,53.6064035980127,54.5991147757537,55.5918259534947,56.5845371312357,
57.5772483089767,57.6659681729845),.UNSPECIFIED.);
#1452=B_SPLINE_CURVE_WITH_KNOTS('',3,(#18684,#18685,#18686,#18687,#18688,
#18689,#18690,#18691,#18692,#18693,#18694,#18695,#18696,#18697,#18698,#18699,
#18700,#18701,#18702,#18703,#18704,#18705),.UNSPECIFIED.,.F.,.F.,(4,3,3,
3,3,3,3,4),(-66.9247834919266,-66.4553311318613,-65.4634605179529,-64.4715899040445,
-63.4797192901362,-62.4878486762278,-61.4959780623194,-60.641598184747),
 .UNSPECIFIED.);
#1453=B_SPLINE_CURVE_WITH_KNOTS('',3,(#18706,#18707,#18708,#18709,#18710,
#18711,#18712,#18713,#18714,#18715,#18716,#18717,#18718,#18719,#18720,#18721,
#18722,#18723,#18724,#18725,#18726,#18727),.UNSPECIFIED.,.F.,.F.,(4,3,3,
3,3,3,3,4),(57.6659681729845,58.5699594867177,59.5626706644586,60.5553818421996,
61.5480930199406,62.5408041976816,63.5335153754225,63.9491534801641),
 .UNSPECIFIED.);
#1454=B_SPLINE_CURVE_WITH_KNOTS('',3,(#18732,#18733,#18734,#18735,#18736,
#18737,#18738,#18739,#18740,#18741,#18742,#18743,#18744,#18745,#18746,#18747,
#18748,#18749,#18750,#18751,#18752,#18753),.UNSPECIFIED.,.F.,.F.,(4,3,3,
3,3,3,3,4),(-73.2079687991062,-72.4065548153116,-71.4146842014032,-70.4228135874948,
-69.4309429735864,-68.4390723596781,-67.4472017457697,-66.9247834919266),
 .UNSPECIFIED.);
#1455=B_SPLINE_CURVE_WITH_KNOTS('',3,(#18754,#18755,#18756,#18757,#18758,
#18759,#18760,#18761,#18762,#18763,#18764,#18765,#18766,#18767,#18768,#18769,
#18770,#18771,#18772,#18773,#18774,#18775),.UNSPECIFIED.,.F.,.F.,(4,3,3,
3,3,3,3,4),(63.9491534801641,64.5262265531635,65.5189377309045,66.5116489086455,
67.5043600863864,68.4970712641274,69.4897824418684,70.2323387873437),
 .UNSPECIFIED.);
#1456=B_SPLINE_CURVE_WITH_KNOTS('',3,(#18780,#18781,#18782,#18783,#18784,
#18785,#18786,#18787,#18788,#18789,#18790,#18791,#18792,#18793,#18794,#18795,
#18796,#18797,#18798,#18799,#18800,#18801,#18802,#18803,#18804),
 .UNSPECIFIED.,.F.,.F.,(4,3,3,3,3,3,3,3,4),(-79.4911541062857,-79.3496491126702,
-78.3577784987618,-77.3659078848535,-76.3740372709451,-75.3821666570367,
-74.3902960431283,-73.3984254292199,-73.2079687991062),.UNSPECIFIED.);
#1457=B_SPLINE_CURVE_WITH_KNOTS('',3,(#18805,#18806,#18807,#18808,#18809,
#18810,#18811,#18812,#18813,#18814,#18815,#18816,#18817,#18818,#18819,#18820,
#18821,#18822,#18823,#18824,#18825,#18826,#18827,#18828,#18829),
 .UNSPECIFIED.,.F.,.F.,(4,3,3,3,3,3,3,3,4),(70.2323387873437,70.4824936196094,
71.4752047973503,72.4679159750913,73.4606271528323,74.4533383305733,75.4460495083142,
76.4387606860552,76.5155240945233),.UNSPECIFIED.);
#1458=B_SPLINE_CURVE_WITH_KNOTS('',3,(#18834,#18835,#18836,#18837,#18838,
#18839,#18840,#18841,#18842,#18843,#18844,#18845,#18846,#18847,#18848,#18849,
#18850,#18851,#18852,#18853,#18854,#18855),.UNSPECIFIED.,.F.,.F.,(4,3,3,
3,3,3,3,4),(-85.7743394134653,-85.3008727961205,-84.3090021822121,-83.3171315683037,
-82.3252609543953,-81.333390340487,-80.3415197265786,-79.4911541062857),
 .UNSPECIFIED.);
#1459=B_SPLINE_CURVE_WITH_KNOTS('',3,(#18856,#18857,#18858,#18859,#18860,
#18861,#18862,#18863,#18864,#18865,#18866,#18867,#18868,#18869,#18870,#18871,
#18872,#18873,#18874,#18875,#18876,#18877),.UNSPECIFIED.,.F.,.F.,(4,3,3,
3,3,3,3,4),(76.5155240945233,77.4314718637962,78.4241830415372,79.4168942192782,
80.4096053970191,81.4023165747601,82.3950277525011,82.7987094017029),
 .UNSPECIFIED.);
#1460=B_SPLINE_CURVE_WITH_KNOTS('',3,(#18882,#18883,#18884,#18885,#18886,
#18887,#18888,#18889,#18890,#18891,#18892,#18893,#18894,#18895,#18896,#18897,
#18898,#18899,#18900,#18901,#18902,#18903),.UNSPECIFIED.,.F.,.F.,(4,3,3,
3,3,3,3,4),(-92.0575247206449,-91.2520964795708,-90.2602258656624,-89.268355251754,
-88.2764846378456,-87.2846140239373,-86.2927434100289,-85.7743394134653),
 .UNSPECIFIED.);
#1461=B_SPLINE_CURVE_WITH_KNOTS('',3,(#18904,#18905,#18906,#18907,#18908,
#18909,#18910,#18911,#18912,#18913,#18914,#18915,#18916,#18917,#18918,#18919,
#18920,#18921,#18922,#18923,#18924,#18925),.UNSPECIFIED.,.F.,.F.,(4,3,3,
3,3,3,3,4),(82.7987094017029,83.3877389302421,84.380450107983,85.373161285724,
86.365872463465,87.358583641206,88.351294818947,89.0818947088825),
 .UNSPECIFIED.);
#1462=B_SPLINE_CURVE_WITH_KNOTS('',3,(#18931,#18932,#18933,#18934,#18935,
#18936,#18937,#18938,#18939,#18940),.UNSPECIFIED.,.F.,.F.,(4,1,1,1,1,1,
1,4),(103.672557568463,103.858999941297,104.850870555206,105.842741169114,
106.834611783022,107.826482396931,108.818353010839,109.810223624748),
 .UNSPECIFIED.);
#1463=B_SPLINE_CURVE_WITH_KNOTS('',3,(#18943,#18944,#18945,#18946,#18947,
#18948,#18949,#18950),.UNSPECIFIED.,.F.,.F.,(4,1,1,1,1,4),(103.672557568463,
104.600461793276,105.593172971017,106.585884148758,107.578595326499,108.57130650424),
 .UNSPECIFIED.);
#1464=B_SPLINE_CURVE_WITH_KNOTS('',3,(#18955,#18956,#18957,#18958,#18959,
#18960,#18961,#18962,#18963,#18964),.UNSPECIFIED.,.F.,.F.,(4,1,1,1,1,1,
1,4),(97.3893722612836,97.9077762578471,98.8996468717555,99.8915174856638,
100.883388099572,101.875258713481,102.867129327389,103.672557568463),
 .UNSPECIFIED.);
#1465=B_SPLINE_CURVE_WITH_KNOTS('',3,(#18965,#18966,#18967,#18968,#18969,
#18970,#18971,#18972,#18973,#18974,#18975),.UNSPECIFIED.,.F.,.F.,(4,1,1,
1,1,1,1,1,4),(97.3893722612836,97.6514835490889,98.6441947268299,99.6369059045709,
100.629617082312,101.622328260053,102.615039437794,103.607750615535,103.672557568463),
 .UNSPECIFIED.);
#1466=B_SPLINE_CURVE_WITH_KNOTS('',3,(#18980,#18981,#18982,#18983,#18984,
#18985,#18986,#18987,#18988,#18989),.UNSPECIFIED.,.F.,.F.,(4,1,1,1,1,1,
1,4),(91.106186954104,91.9565525743968,92.9484231883052,93.9402938022136,
94.9321644161219,95.9240350300303,96.9159056439387,97.3893722612836),
 .UNSPECIFIED.);
#1467=B_SPLINE_CURVE_WITH_KNOTS('',3,(#18990,#18991,#18992,#18993,#18994,
#18995,#18996,#18997,#18998,#18999),.UNSPECIFIED.,.F.,.F.,(4,1,1,1,1,1,
1,4),(91.106186954104,91.6952164826431,92.687927660384,93.680638838125,
94.673350015866,95.666061193607,96.658772371348,97.3893722612836),
 .UNSPECIFIED.);
#1468=B_SPLINE_CURVE_WITH_KNOTS('',3,(#19004,#19005,#19006,#19007,#19008,
#19009,#19010,#19011,#19012,#19013,#19014),.UNSPECIFIED.,.F.,.F.,(4,1,1,
1,1,1,1,1,4),(84.8230016469244,85.0134582770382,86.0053288909465,86.9971995048549,
87.9890701187633,88.9809407326717,89.9728113465801,90.9646819604884,91.106186954104),
 .UNSPECIFIED.);
#1469=B_SPLINE_CURVE_WITH_KNOTS('',3,(#19015,#19016,#19017,#19018,#19019,
#19020,#19021,#19022,#19023,#19024),.UNSPECIFIED.,.F.,.F.,(4,1,1,1,1,1,
1,4),(84.8230016469244,85.7389494161972,86.7316605939382,87.7243717716792,
88.7170829494201,89.7097941271611,90.7025053049021,91.106186954104),
 .UNSPECIFIED.);
#1470=B_SPLINE_CURVE_WITH_KNOTS('',3,(#19029,#19030,#19031,#19032,#19033,
#19034,#19035,#19036,#19037,#19038),.UNSPECIFIED.,.F.,.F.,(4,1,1,1,1,1,
1,4),(78.5398163397448,79.0622345935879,80.0541052074963,81.0459758214047,
82.037846435313,83.0297170492214,84.0215876631298,84.8230016469244),
 .UNSPECIFIED.);
#1471=B_SPLINE_CURVE_WITH_KNOTS('',3,(#19039,#19040,#19041,#19042,#19043,
#19044,#19045,#19046,#19047,#19048,#19049),.UNSPECIFIED.,.F.,.F.,(4,1,1,
1,1,1,1,1,4),(78.5398163397448,78.7899711720104,79.7826823497514,80.7753935274923,
81.7681047052333,82.7608158829743,83.7535270607153,84.7462382384562,84.8230016469244),
 .UNSPECIFIED.);
#1472=B_SPLINE_CURVE_WITH_KNOTS('',3,(#19054,#19055,#19056,#19057,#19058,
#19059,#19060,#19061,#19062,#19063),.UNSPECIFIED.,.F.,.F.,(4,1,1,1,1,1,
1,4),(72.2566310325652,73.1110109101376,74.102881524046,75.0947521379544,
76.0866227518628,77.0784933657711,78.0703639796795,78.5398163397448),
 .UNSPECIFIED.);
#1473=B_SPLINE_CURVE_WITH_KNOTS('',3,(#19064,#19065,#19066,#19067,#19068,
#19069,#19070,#19071,#19072,#19073),.UNSPECIFIED.,.F.,.F.,(4,1,1,1,1,1,
1,4),(72.2566310325652,72.8337041055645,73.8264152833055,74.8191264610465,
75.8118376387874,76.8045488165284,77.7972599942694,78.5398163397448),
 .UNSPECIFIED.);
#1474=B_SPLINE_CURVE_WITH_KNOTS('',3,(#19078,#19079,#19080,#19081,#19082,
#19083,#19084,#19085,#19086,#19087,#19088),.UNSPECIFIED.,.F.,.F.,(4,1,1,
1,1,1,1,1,4),(65.9734457253856,66.167916612779,67.1597872266874,68.1516578405957,
69.1435284545041,70.1353990684125,71.1272696823209,72.1191402962293,72.2566310325652),
 .UNSPECIFIED.);
#1475=B_SPLINE_CURVE_WITH_KNOTS('',3,(#19089,#19090,#19091,#19092,#19093,
#19094,#19095,#19096,#19097,#19098),.UNSPECIFIED.,.F.,.F.,(4,1,1,1,1,1,
1,4),(65.9734457253856,66.8774370391187,67.8701482168596,68.8628593946006,
69.8555705723416,70.8482817500825,71.8409929278235,72.2566310325652),
 .UNSPECIFIED.);
#1476=B_SPLINE_CURVE_WITH_KNOTS('',3,(#19103,#19104,#19105,#19106,#19107,
#19108,#19109,#19110,#19111,#19112),.UNSPECIFIED.,.F.,.F.,(4,1,1,1,1,1,
1,4),(59.6902604182061,60.2166929293287,61.2085635432371,62.2004341571455,
63.1923047710539,64.1841753849622,65.1760459988706,65.9734457253856),
 .UNSPECIFIED.);
#1477=B_SPLINE_CURVE_WITH_KNOTS('',3,(#19113,#19114,#19115,#19116,#19117,
#19118,#19119,#19120,#19121,#19122,#19123),.UNSPECIFIED.,.F.,.F.,(4,1,1,
1,1,1,1,1,4),(59.690260418206,59.9284587949318,60.9211699726728,61.9138811504138,
62.9065923281547,63.8993035058957,64.8920146836367,65.8847258613777,65.9734457253856),
 .UNSPECIFIED.);
#1478=B_SPLINE_CURVE_WITH_KNOTS('',3,(#19128,#19129,#19130,#19131,#19132,
#19133,#19134,#19135,#19136,#19137),.UNSPECIFIED.,.F.,.F.,(4,1,1,1,1,1,
1,4),(53.4070751110265,54.2654692458785,55.2573398597868,56.2492104736952,
57.2410810876036,58.232951701512,59.2248223154203,59.6902604182061),
 .UNSPECIFIED.);
#1479=B_SPLINE_CURVE_WITH_KNOTS('',3,(#19138,#19139,#19140,#19141,#19142,
#19143,#19144,#19145,#19146,#19147),.UNSPECIFIED.,.F.,.F.,(4,1,1,1,1,1,
1,4),(53.4070751110264,53.972191728486,54.9649029062269,55.9576140839679,
56.9503252617089,57.9430364394499,58.9357476171908,59.690260418206),
 .UNSPECIFIED.);
#1480=B_SPLINE_CURVE_WITH_KNOTS('',3,(#19152,#19153,#19154,#19155,#19156,
#19157,#19158,#19159,#19160,#19161,#19162),.UNSPECIFIED.,.F.,.F.,(4,1,1,
1,1,1,1,1,4),(47.1238898038469,47.3223749485198,48.3142455624282,49.3061161763366,
50.2979867902449,51.2898574041533,52.2817280180617,53.2735986319701,53.4070751110265),
 .UNSPECIFIED.);
#1481=B_SPLINE_CURVE_WITH_KNOTS('',3,(#19163,#19164,#19165,#19166,#19167,
#19168,#19169,#19170,#19171,#19172),.UNSPECIFIED.,.F.,.F.,(4,1,1,1,1,1,
1,4),(47.1238898038468,48.0159246620401,49.0086358397811,50.001347017522,
50.994058195263,51.986769373004,52.979480550745,53.4070751110264),
 .UNSPECIFIED.);
#1482=B_SPLINE_CURVE_WITH_KNOTS('',3,(#19177,#19178,#19179,#19180,#19181,
#19182,#19183,#19184,#19185,#19186),.UNSPECIFIED.,.F.,.F.,(4,1,1,1,1,1,
1,4),(40.8407044966673,41.3711512650695,42.3630218789779,43.3548924928863,
44.3467631067947,45.3386337207031,46.3305043346114,47.1238898038469),
 .UNSPECIFIED.);
#1483=B_SPLINE_CURVE_WITH_KNOTS('',3,(#19187,#19188,#19189,#19190,#19191,
#19192,#19193,#19194,#19195,#19196,#19197),.UNSPECIFIED.,.F.,.F.,(4,1,1,
1,1,1,1,1,4),(40.8407044966672,41.0669464178533,42.0596575955942,43.0523687733352,
44.0450799510762,45.0377911288172,46.0305023065581,47.0232134842991,47.1238898038468),
 .UNSPECIFIED.);
#1484=B_SPLINE_CURVE_WITH_KNOTS('',3,(#19202,#19203,#19204,#19205,#19206,
#19207,#19208,#19209,#19210,#19211),.UNSPECIFIED.,.F.,.F.,(4,1,1,1,1,1,
1,4),(34.5575191894877,35.4199275816193,36.4117981955277,37.403668809436,
38.3955394233444,39.3874100372528,40.3792806511612,40.8407044966673),
 .UNSPECIFIED.);
#1485=B_SPLINE_CURVE_WITH_KNOTS('',3,(#19212,#19213,#19214,#19215,#19216,
#19217,#19218,#19219,#19220,#19221),.UNSPECIFIED.,.F.,.F.,(4,1,1,1,1,1,
1,4),(34.5575191894876,35.1106793514074,36.1033905291484,37.0961017068893,
38.0888128846303,39.0815240623713,40.0742352401123,40.8407044966672),
 .UNSPECIFIED.);
#1486=B_SPLINE_CURVE_WITH_KNOTS('',3,(#19226,#19227,#19228,#19229,#19230,
#19231,#19232,#19233,#19234,#19235,#19236),.UNSPECIFIED.,.F.,.F.,(4,1,1,
1,1,1,1,1,4),(28.2743338823081,28.4768332842606,29.468703898169,30.4605745120774,
31.4524451259858,32.4443157398941,33.4361863538025,34.4280569677109,34.5575191894877),
 .UNSPECIFIED.);
#1487=B_SPLINE_CURVE_WITH_KNOTS('',3,(#19237,#19238,#19239,#19240,#19241,
#19242,#19243,#19244,#19245,#19246),.UNSPECIFIED.,.F.,.F.,(4,1,1,1,1,1,
1,4),(28.2743338823081,29.1544122849615,30.1471234627025,31.1398346404435,
32.1325458181845,33.1252569959254,34.1179681736664,34.5575191894876),
 .UNSPECIFIED.);
#1488=B_SPLINE_CURVE_WITH_KNOTS('',3,(#19251,#19252,#19253,#19254,#19255,
#19256,#19257,#19258,#19259,#19260),.UNSPECIFIED.,.F.,.F.,(4,1,1,1,1,1,
1,4),(21.9911485751285,22.5256096008104,23.5174802147187,24.5093508286271,
25.5012214425355,26.4930920564439,27.4849626703523,28.2743338823081),
 .UNSPECIFIED.);
#1489=B_SPLINE_CURVE_WITH_KNOTS('',3,(#19261,#19262,#19263,#19264,#19265,
#19266,#19267,#19268,#19269,#19270,#19271),.UNSPECIFIED.,.F.,.F.,(4,1,1,
1,1,1,1,1,4),(21.9911485751285,22.2054340407747,23.1981452185157,24.1908563962566,
25.1835675739976,26.1762787517386,27.1689899294796,28.1617011072206,28.2743338823081),
 .UNSPECIFIED.);
#1490=B_SPLINE_CURVE_WITH_KNOTS('',3,(#19276,#19277,#19278,#19279,#19280,
#19281,#19282,#19283,#19284,#19285),.UNSPECIFIED.,.F.,.F.,(4,1,1,1,1,1,
1,4),(15.7079632679489,16.5743859173601,17.5662565312685,18.5581271451769,
19.5499977590852,20.5418683729936,21.533738986902,21.9911485751285),
 .UNSPECIFIED.);
#1491=B_SPLINE_CURVE_WITH_KNOTS('',3,(#19286,#19287,#19288,#19289,#19290,
#19291,#19292,#19293,#19294,#19295),.UNSPECIFIED.,.F.,.F.,(4,1,1,1,1,1,
1,4),(15.7079632679489,16.2491669743288,17.2418781520698,18.2345893298108,
19.2273005075518,20.2200116852927,21.2127228630337,21.9911485751285),
 .UNSPECIFIED.);
#1492=B_SPLINE_CURVE_WITH_KNOTS('',3,(#19298,#19299,#19300,#19301,#19302,
#19303,#19304,#19305,#19306,#19307,#19308,#19309,#19310,#19311,#19312,#19313,
#19314,#19315,#19316,#19317,#19318,#19319,#19320,#19321,#19322,#19323,#19324,
#19325,#19326,#19327,#19328,#19329,#19330,#19331,#19332,#19333,#19334,#19335,
#19336,#19337,#19338,#19339,#19340,#19341,#19342,#19343,#19344,#19345,#19346,
#19347,#19348,#19349,#19350,#19351,#19352,#19353,#19354,#19355,#19356,#19357,
#19358,#19359,#19360,#19361,#19362,#19363,#19364,#19365,#19366,#19367,#19368,
#19369,#19370,#19371,#19372,#19373,#19374,#19375,#19376,#19377,#19378,#19379,
#19380,#19381,#19382,#19383,#19384,#19385,#19386,#19387,#19388,#19389,#19390,
#19391,#19392,#19393,#19394,#19395,#19396,#19397,#19398,#19399,#19400,#19401,
#19402,#19403,#19404,#19405,#19406,#19407,#19408,#19409,#19410,#19411,#19412,
#19413,#19414,#19415,#19416,#19417,#19418,#19419,#19420,#19421,#19422,#19423,
#19424,#19425,#19426,#19427,#19428,#19429,#19430,#19431,#19432,#19433,#19434,
#19435,#19436,#19437,#19438,#19439,#19440,#19441,#19442,#19443,#19444,#19445,
#19446,#19447,#19448,#19449,#19450,#19451,#19452,#19453,#19454,#19455,#19456,
#19457,#19458,#19459,#19460,#19461,#19462,#19463,#19464,#19465,#19466,#19467,
#19468,#19469,#19470,#19471,#19472,#19473,#19474,#19475,#19476,#19477,#19478,
#19479,#19480,#19481,#19482,#19483,#19484,#19485,#19486,#19487,#19488,#19489,
#19490,#19491,#19492,#19493,#19494,#19495,#19496,#19497,#19498,#19499,#19500,
#19501,#19502,#19503,#19504,#19505,#19506,#19507,#19508,#19509,#19510,#19511,
#19512,#19513,#19514,#19515,#19516,#19517),.UNSPECIFIED.,.F.,.F.,(4,3,3,
3,3,3,3,3,3,3,3,3,3,3,3,3,3,3,3,3,3,3,3,3,3,3,3,3,3,3,3,3,3,3,3,3,3,3,3,
3,3,3,3,3,3,3,3,3,3,3,3,3,3,3,3,3,3,3,3,3,3,3,3,3,3,3,3,3,3,3,3,3,3,4),
(-1.5115530493723,-1.48679433039677,-1.46137997144481,-1.44936627203976,
-1.44203978844916,-1.43723948275662,-1.41130482704604,-1.3851425648951,
-1.36907979899106,-1.36528335260342,-1.33883417182409,-1.31251413265359,
-1.29083745680875,-1.27999911888633,-1.27252822943752,-1.26916078096391,
-1.2438409010096,-1.21777622976252,-1.19264806966918,-1.18165449962834,
-1.17500808302858,-1.17140113753098,-1.14461626345551,-1.11752388424601,
-1.09233065043846,-1.08197947093734,-1.07663416157974,-1.07221334700158,
-1.04448214800868,-1.01675094901579,-0.989899829038698,-0.980534050538336,
-0.975142748268706,-0.971473262423844,-0.944367339171939,-0.916829945945447,
-0.889160172398661,-0.878253059899969,-0.87283587922991,-0.869128423226553,
-0.840502786522066,-0.812629809126308,-0.785184824902654,-0.776260550181423,
-0.769615191493828,-0.76539079696697,-0.754625876408607,-0.727617533495154,
-0.699889836956671,-0.672733437279935,-0.663027286995113,-0.658922109894078,
-0.630659562625353,-0.602060824740566,-0.57220527844112,-0.560770556686858,
-0.556383058918736,-0.552005977862112,-0.523133364911618,-0.494697204184849,
-0.482638639542781,-0.454174910522506,-0.448377858002803,-0.443883394073885,
-0.415482165359649,-0.386508614853008,-0.357316612716015,-0.340170191390177,
-0.335377465438287,-0.305918315871394,-0.27645436453335,-0.247645675491356,
-0.226999958751525,-0.219677966288016),.UNSPECIFIED.);
#1493=B_SPLINE_CURVE_WITH_KNOTS('',3,(#19519,#19520,#19521,#19522,#19523,
#19524,#19525,#19526,#19527,#19528,#19529,#19530,#19531,#19532,#19533,#19534,
#19535,#19536,#19537,#19538,#19539,#19540,#19541,#19542,#19543,#19544,#19545,
#19546,#19547,#19548,#19549,#19550,#19551,#19552,#19553,#19554,#19555,#19556,
#19557,#19558,#19559,#19560,#19561,#19562,#19563,#19564,#19565,#19566,#19567,
#19568,#19569,#19570,#19571,#19572,#19573,#19574,#19575,#19576,#19577,#19578,
#19579,#19580,#19581,#19582),.UNSPECIFIED.,.F.,.F.,(4,3,3,3,3,3,3,3,3,3,
3,3,3,3,3,3,3,3,3,3,3,4),(-0.410648750433038,-0.381296088292737,-0.350882391849445,
-0.328072119516976,-0.310964415267624,-0.305842993500878,-0.301661871504881,
-0.274116258800685,-0.259641302519569,-0.231392457082299,-0.202468399947011,
-0.198019208917011,-0.170841895434807,-0.143725312403613,-0.117042212888725,
-0.102411936277635,-0.097195049751494,-0.0935363835720784,-0.0677899334604712,
-0.0424347820407558,-0.0178142542830924,0.),.UNSPECIFIED.);
#1494=B_SPLINE_CURVE_WITH_KNOTS('',3,(#19585,#19586,#19587,#19588,#19589,
#19590,#19591,#19592,#19593,#19594,#19595,#19596,#19597,#19598,#19599,#19600,
#19601,#19602,#19603,#19604,#19605,#19606,#19607,#19608,#19609,#19610,#19611,
#19612,#19613,#19614,#19615),.UNSPECIFIED.,.F.,.F.,(4,3,3,3,3,3,3,3,3,3,
4),(-0.219677966288016,-0.201006229477425,-0.172158028090248,-0.142713390739092,
-0.124874216896705,-0.114789665948937,-0.110082687886506,-0.0803547102951982,
-0.0502957032480209,-0.0203907630638487,0.),.UNSPECIFIED.);
#1495=B_SPLINE_CURVE_WITH_KNOTS('',3,(#20028,#20029,#20030,#20031,#20032,
#20033,#20034,#20035),.UNSPECIFIED.,.F.,.F.,(4,1,1,1,1,4),(11.6150328478182,
12.6069034617266,13.598774075635,14.5906446895433,15.5825153034517,15.7079632679489),
 .UNSPECIFIED.);
#1496=B_SPLINE_CURVE_WITH_KNOTS('',3,(#20036,#20037,#20038,#20039,#20040,
#20041,#20042,#20043,#20044,#20045,#20046,#20047,#20048,#20049,#20050,#20051,
#20052,#20053,#20054,#20055,#20056,#20057,#20058,#20059,#20060,#20061,#20062,
#20063,#20064,#20065,#20066,#20067,#20068,#20069,#20070,#20071,#20072,#20073,
#20074,#20075,#20076,#20077,#20078,#20079,#20080,#20081,#20082,#20083,#20084,
#20085,#20086,#20087,#20088,#20089,#20090,#20091,#20092,#20093,#20094,#20095,
#20096,#20097,#20098,#20099,#20100,#20101,#20102,#20103,#20104,#20105,#20106,
#20107,#20108,#20109,#20110,#20111,#20112,#20113,#20114,#20115,#20116,#20117,
#20118,#20119,#20120,#20121,#20122,#20123),.UNSPECIFIED.,.F.,.F.,(4,3,3,
3,3,3,3,3,3,3,3,3,3,3,3,3,3,3,3,3,3,3,3,3,3,3,3,3,3,4),(-0.552745378375041,
-0.527830263536694,-0.498419933292456,-0.482944277728704,-0.477004703287069,
-0.471889411648522,-0.442842142020847,-0.418838054802294,-0.408336266644177,
-0.40199148464016,-0.397446251891128,-0.369139848009071,-0.341087780585202,
-0.313931322984348,-0.298150853306366,-0.293754274173184,-0.266922432864957,
-0.250809444272419,-0.223433348051691,-0.19550417954523,-0.19139998392206,
-0.164790719651446,-0.138164593558308,-0.11192170155777,-0.0979314888630491,
-0.0936568444848153,-0.0680692021908508,-0.0428602319276656,-0.0184469101431373,
0.),.UNSPECIFIED.);
#1497=B_SPLINE_CURVE_WITH_KNOTS('',3,(#20124,#20125,#20126,#20127,#20128,
#20129,#20130,#20131,#20132,#20133,#20134,#20135,#20136,#20137,#20138,#20139,
#20140,#20141,#20142),.UNSPECIFIED.,.F.,.F.,(4,3,3,3,3,3,4),(-96.6808425304193,
-96.2114495491126,-95.2195789352043,-94.2277083212959,-93.2358377073875,
-92.2439670934791,-92.0575247206449),.UNSPECIFIED.);
#1498=B_SPLINE_CURVE_WITH_KNOTS('',3,(#20145,#20146,#20147,#20148,#20149,
#20150,#20151,#20152,#20153),.UNSPECIFIED.,.F.,.F.,(4,1,1,1,1,1,4),(10.3761157273101,
11.2856110856239,12.2783222633649,13.2710334411059,14.2637446188469,15.2564557965878,
15.7079632679489),.UNSPECIFIED.);
#1499=B_SPLINE_CURVE_WITH_KNOTS('',3,(#20571,#20572,#20573,#20574,#20575,
#20576,#20577,#20578,#20579,#20580,#20581,#20582,#20583,#20584,#20585,#20586,
#20587,#20588,#20589,#20590,#20591,#20592),.UNSPECIFIED.,.F.,.F.,(4,3,3,
3,3,3,3,4),(89.0818947088825,89.3440059966879,90.3367171744289,91.3294283521699,
92.3221395299109,93.3148507076518,94.3075618853928,94.6122043555102),
 .UNSPECIFIED.);
#1500=B_SPLINE_CURVE_WITH_KNOTS('',3,(#20593,#20594,#20595,#20596,#20597,
#20598,#20599,#20600,#20601,#20602,#20603,#20604,#20605,#20606,#20607,#20608,
#20609,#20610,#20611,#20612,#20613,#20614,#20615,#20616,#20617,#20618,#20619,
#20620,#20621,#20622,#20623,#20624,#20625,#20626,#20627,#20628,#20629,#20630,
#20631,#20632,#20633,#20634,#20635,#20636,#20637,#20638,#20639,#20640,#20641,
#20642,#20643,#20644,#20645,#20646,#20647,#20648,#20649,#20650,#20651,#20652,
#20653,#20654,#20655,#20656,#20657,#20658,#20659,#20660,#20661,#20662,#20663,
#20664,#20665,#20666,#20667,#20668,#20669,#20670,#20671,#20672,#20673,#20674,
#20675,#20676,#20677,#20678,#20679,#20680),.UNSPECIFIED.,.F.,.F.,(4,3,3,
3,3,3,3,3,3,3,3,3,3,3,3,3,3,3,3,3,3,3,3,3,3,3,3,3,3,4),(-0.555272788399392,
-0.535208229286056,-0.51046000550438,-0.495927663091087,-0.490771565699598,
-0.464551573131573,-0.44160907963455,-0.431518091480653,-0.425427657470475,
-0.420791193383041,-0.394188077983384,-0.365893964776387,-0.344673379871139,
-0.328757941192203,-0.324434111993057,-0.296521822210165,-0.281011625155395,
-0.254049889550291,-0.226554106924644,-0.220947145848259,-0.216688100237889,
-0.188737539857684,-0.160250957640402,-0.131525362881473,-0.114279480489655,
-0.109581292141837,-0.0801117384511396,-0.0505679692714886,-0.0215915474943119,
0.),.UNSPECIFIED.);
#1905=LINE('',#18209,#2361);
#1906=LINE('',#18233,#2362);
#1907=LINE('',#18281,#2363);
#1908=LINE('',#18329,#2364);
#1909=LINE('',#18383,#2365);
#1910=LINE('',#18431,#2366);
#1911=LINE('',#18479,#2367);
#1912=LINE('',#18533,#2368);
#1913=LINE('',#18581,#2369);
#1914=LINE('',#18629,#2370);
#1915=LINE('',#18683,#2371);
#1916=LINE('',#18731,#2372);
#1917=LINE('',#18779,#2373);
#1918=LINE('',#18833,#2374);
#1919=LINE('',#18881,#2375);
#1920=LINE('',#18929,#2376);
#1921=LINE('',#18954,#2377);
#1922=LINE('',#18979,#2378);
#1923=LINE('',#19003,#2379);
#1924=LINE('',#19028,#2380);
#1925=LINE('',#19053,#2381);
#1926=LINE('',#19077,#2382);
#1927=LINE('',#19102,#2383);
#1928=LINE('',#19127,#2384);
#1929=LINE('',#19151,#2385);
#1930=LINE('',#19176,#2386);
#1931=LINE('',#19201,#2387);
#1932=LINE('',#19225,#2388);
#1933=LINE('',#19250,#2389);
#1934=LINE('',#19275,#2390);
#1935=LINE('',#19617,#2391);
#1936=LINE('',#20685,#2392);
#1937=LINE('',#20687,#2393);
#1938=LINE('',#20689,#2394);
#1939=LINE('',#20690,#2395);
#1940=LINE('',#20693,#2396);
#1941=LINE('',#20695,#2397);
#1942=LINE('',#20696,#2398);
#1943=LINE('',#20699,#2399);
#1944=LINE('',#20701,#2400);
#1945=LINE('',#20702,#2401);
#1946=LINE('',#20705,#2402);
#1947=LINE('',#20707,#2403);
#1948=LINE('',#20708,#2404);
#1949=LINE('',#20711,#2405);
#1950=LINE('',#20713,#2406);
#1951=LINE('',#20714,#2407);
#1952=LINE('',#20716,#2408);
#1953=LINE('',#20717,#2409);
#1954=LINE('',#20724,#2410);
#2361=VECTOR('',#8071,3.);
#2362=VECTOR('',#8076,3.);
#2363=VECTOR('',#8079,3.);
#2364=VECTOR('',#8082,3.);
#2365=VECTOR('',#8085,3.);
#2366=VECTOR('',#8088,3.);
#2367=VECTOR('',#8091,3.);
#2368=VECTOR('',#8094,3.);
#2369=VECTOR('',#8097,3.);
#2370=VECTOR('',#8100,3.);
#2371=VECTOR('',#8103,3.);
#2372=VECTOR('',#8106,3.);
#2373=VECTOR('',#8109,3.);
#2374=VECTOR('',#8112,3.);
#2375=VECTOR('',#8115,3.);
#2376=VECTOR('',#8118,2.37175);
#2377=VECTOR('',#8123,2.37175);
#2378=VECTOR('',#8126,2.37175);
#2379=VECTOR('',#8129,2.37175);
#2380=VECTOR('',#8132,2.37175);
#2381=VECTOR('',#8135,2.37175);
#2382=VECTOR('',#8138,2.37175);
#2383=VECTOR('',#8141,2.37175);
#2384=VECTOR('',#8144,2.37175);
#2385=VECTOR('',#8147,2.37175);
#2386=VECTOR('',#8150,2.37175);
#2387=VECTOR('',#8153,2.37175);
#2388=VECTOR('',#8156,2.37175);
#2389=VECTOR('',#8159,2.37175);
#2390=VECTOR('',#8162,2.37175);
#2391=VECTOR('',#8167,2.5);
#2392=VECTOR('',#8178,10.);
#2393=VECTOR('',#8179,10.);
#2394=VECTOR('',#8180,10.);
#2395=VECTOR('',#8181,10.);
#2396=VECTOR('',#8184,10.);
#2397=VECTOR('',#8185,10.);
#2398=VECTOR('',#8186,10.);
#2399=VECTOR('',#8189,10.);
#2400=VECTOR('',#8190,10.);
#2401=VECTOR('',#8191,10.);
#2402=VECTOR('',#8194,10.);
#2403=VECTOR('',#8195,10.);
#2404=VECTOR('',#8196,10.);
#2405=VECTOR('',#8199,10.);
#2406=VECTOR('',#8200,10.);
#2407=VECTOR('',#8201,10.);
#2408=VECTOR('',#8204,10.);
#2409=VECTOR('',#8205,10.);
#2410=VECTOR('',#8214,5.);
#2919=VERTEX_POINT('',#18207);
#2920=VERTEX_POINT('',#18208);
#2921=VERTEX_POINT('',#18210);
#2922=VERTEX_POINT('',#18221);
#2923=VERTEX_POINT('',#18231);
#2924=VERTEX_POINT('',#18232);
#2925=VERTEX_POINT('',#18279);
#2926=VERTEX_POINT('',#18280);
#2927=VERTEX_POINT('',#18327);
#2928=VERTEX_POINT('',#18328);
#2929=VERTEX_POINT('',#18381);
#2930=VERTEX_POINT('',#18382);
#2931=VERTEX_POINT('',#18429);
#2932=VERTEX_POINT('',#18430);
#2933=VERTEX_POINT('',#18477);
#2934=VERTEX_POINT('',#18478);
#2935=VERTEX_POINT('',#18531);
#2936=VERTEX_POINT('',#18532);
#2937=VERTEX_POINT('',#18579);
#2938=VERTEX_POINT('',#18580);
#2939=VERTEX_POINT('',#18627);
#2940=VERTEX_POINT('',#18628);
#2941=VERTEX_POINT('',#18681);
#2942=VERTEX_POINT('',#18682);
#2943=VERTEX_POINT('',#18729);
#2944=VERTEX_POINT('',#18730);
#2945=VERTEX_POINT('',#18777);
#2946=VERTEX_POINT('',#18778);
#2947=VERTEX_POINT('',#18831);
#2948=VERTEX_POINT('',#18832);
#2949=VERTEX_POINT('',#18879);
#2950=VERTEX_POINT('',#18880);
#2951=VERTEX_POINT('',#18927);
#2952=VERTEX_POINT('',#18928);
#2953=VERTEX_POINT('',#18930);
#2954=VERTEX_POINT('',#18941);
#2955=VERTEX_POINT('',#18952);
#2956=VERTEX_POINT('',#18953);
#2957=VERTEX_POINT('',#18977);
#2958=VERTEX_POINT('',#18978);
#2959=VERTEX_POINT('',#19001);
#2960=VERTEX_POINT('',#19002);
#2961=VERTEX_POINT('',#19026);
#2962=VERTEX_POINT('',#19027);
#2963=VERTEX_POINT('',#19051);
#2964=VERTEX_POINT('',#19052);
#2965=VERTEX_POINT('',#19075);
#2966=VERTEX_POINT('',#19076);
#2967=VERTEX_POINT('',#19100);
#2968=VERTEX_POINT('',#19101);
#2969=VERTEX_POINT('',#19125);
#2970=VERTEX_POINT('',#19126);
#2971=VERTEX_POINT('',#19149);
#2972=VERTEX_POINT('',#19150);
#2973=VERTEX_POINT('',#19174);
#2974=VERTEX_POINT('',#19175);
#2975=VERTEX_POINT('',#19199);
#2976=VERTEX_POINT('',#19200);
#2977=VERTEX_POINT('',#19223);
#2978=VERTEX_POINT('',#19224);
#2979=VERTEX_POINT('',#19248);
#2980=VERTEX_POINT('',#19249);
#2981=VERTEX_POINT('',#19273);
#2982=VERTEX_POINT('',#19274);
#2983=VERTEX_POINT('',#19297);
#2984=VERTEX_POINT('',#19518);
#2985=VERTEX_POINT('',#19583);
#2986=VERTEX_POINT('',#19616);
#2987=VERTEX_POINT('',#20027);
#2988=VERTEX_POINT('',#20144);
#2989=VERTEX_POINT('',#20683);
#2990=VERTEX_POINT('',#20684);
#2991=VERTEX_POINT('',#20686);
#2992=VERTEX_POINT('',#20688);
#2993=VERTEX_POINT('',#20692);
#2994=VERTEX_POINT('',#20694);
#2995=VERTEX_POINT('',#20698);
#2996=VERTEX_POINT('',#20700);
#2997=VERTEX_POINT('',#20704);
#2998=VERTEX_POINT('',#20706);
#2999=VERTEX_POINT('',#20710);
#3000=VERTEX_POINT('',#20712);
#3001=VERTEX_POINT('',#20720);
#3002=VERTEX_POINT('',#20723);
#3783=EDGE_CURVE('',#2919,#2920,#1905,.T.);
#3784=EDGE_CURVE('',#2919,#2921,#1432,.T.);
#3785=EDGE_CURVE('',#2921,#2922,#1147,.F.);
#3786=EDGE_CURVE('',#2922,#2920,#1433,.T.);
#3787=EDGE_CURVE('',#2923,#2924,#1906,.T.);
#3788=EDGE_CURVE('',#2923,#2919,#1434,.T.);
#3789=EDGE_CURVE('',#2920,#2924,#1435,.T.);
#3790=EDGE_CURVE('',#2925,#2926,#1907,.T.);
#3791=EDGE_CURVE('',#2925,#2923,#1436,.T.);
#3792=EDGE_CURVE('',#2924,#2926,#1437,.T.);
#3793=EDGE_CURVE('',#2927,#2928,#1908,.T.);
#3794=EDGE_CURVE('',#2927,#2925,#1438,.T.);
#3795=EDGE_CURVE('',#2926,#2928,#1439,.T.);
#3796=EDGE_CURVE('',#2929,#2930,#1909,.T.);
#3797=EDGE_CURVE('',#2929,#2927,#1440,.T.);
#3798=EDGE_CURVE('',#2928,#2930,#1441,.T.);
#3799=EDGE_CURVE('',#2931,#2932,#1910,.T.);
#3800=EDGE_CURVE('',#2931,#2929,#1442,.T.);
#3801=EDGE_CURVE('',#2930,#2932,#1443,.T.);
#3802=EDGE_CURVE('',#2933,#2934,#1911,.T.);
#3803=EDGE_CURVE('',#2933,#2931,#1444,.T.);
#3804=EDGE_CURVE('',#2932,#2934,#1445,.T.);
#3805=EDGE_CURVE('',#2935,#2936,#1912,.T.);
#3806=EDGE_CURVE('',#2935,#2933,#1446,.T.);
#3807=EDGE_CURVE('',#2934,#2936,#1447,.T.);
#3808=EDGE_CURVE('',#2937,#2938,#1913,.T.);
#3809=EDGE_CURVE('',#2937,#2935,#1448,.T.);
#3810=EDGE_CURVE('',#2936,#2938,#1449,.T.);
#3811=EDGE_CURVE('',#2939,#2940,#1914,.T.);
#3812=EDGE_CURVE('',#2939,#2937,#1450,.T.);
#3813=EDGE_CURVE('',#2938,#2940,#1451,.T.);
#3814=EDGE_CURVE('',#2941,#2942,#1915,.T.);
#3815=EDGE_CURVE('',#2941,#2939,#1452,.T.);
#3816=EDGE_CURVE('',#2940,#2942,#1453,.T.);
#3817=EDGE_CURVE('',#2943,#2944,#1916,.T.);
#3818=EDGE_CURVE('',#2943,#2941,#1454,.T.);
#3819=EDGE_CURVE('',#2942,#2944,#1455,.T.);
#3820=EDGE_CURVE('',#2945,#2946,#1917,.T.);
#3821=EDGE_CURVE('',#2945,#2943,#1456,.T.);
#3822=EDGE_CURVE('',#2944,#2946,#1457,.T.);
#3823=EDGE_CURVE('',#2947,#2948,#1918,.T.);
#3824=EDGE_CURVE('',#2947,#2945,#1458,.T.);
#3825=EDGE_CURVE('',#2946,#2948,#1459,.T.);
#3826=EDGE_CURVE('',#2949,#2950,#1919,.T.);
#3827=EDGE_CURVE('',#2949,#2947,#1460,.T.);
#3828=EDGE_CURVE('',#2948,#2950,#1461,.T.);
#3829=EDGE_CURVE('',#2951,#2952,#1920,.T.);
#3830=EDGE_CURVE('',#2951,#2953,#1462,.T.);
#3831=EDGE_CURVE('',#2953,#2954,#1148,.T.);
#3832=EDGE_CURVE('',#2952,#2954,#1463,.T.);
#3833=EDGE_CURVE('',#2955,#2956,#1921,.T.);
#3834=EDGE_CURVE('',#2955,#2951,#1464,.T.);
#3835=EDGE_CURVE('',#2956,#2952,#1465,.T.);
#3836=EDGE_CURVE('',#2957,#2958,#1922,.T.);
#3837=EDGE_CURVE('',#2957,#2955,#1466,.T.);
#3838=EDGE_CURVE('',#2958,#2956,#1467,.T.);
#3839=EDGE_CURVE('',#2959,#2960,#1923,.T.);
#3840=EDGE_CURVE('',#2959,#2957,#1468,.T.);
#3841=EDGE_CURVE('',#2960,#2958,#1469,.T.);
#3842=EDGE_CURVE('',#2961,#2962,#1924,.T.);
#3843=EDGE_CURVE('',#2961,#2959,#1470,.T.);
#3844=EDGE_CURVE('',#2962,#2960,#1471,.T.);
#3845=EDGE_CURVE('',#2963,#2964,#1925,.T.);
#3846=EDGE_CURVE('',#2963,#2961,#1472,.T.);
#3847=EDGE_CURVE('',#2964,#2962,#1473,.T.);
#3848=EDGE_CURVE('',#2965,#2966,#1926,.T.);
#3849=EDGE_CURVE('',#2965,#2963,#1474,.T.);
#3850=EDGE_CURVE('',#2966,#2964,#1475,.T.);
#3851=EDGE_CURVE('',#2967,#2968,#1927,.T.);
#3852=EDGE_CURVE('',#2967,#2965,#1476,.T.);
#3853=EDGE_CURVE('',#2968,#2966,#1477,.T.);
#3854=EDGE_CURVE('',#2969,#2970,#1928,.T.);
#3855=EDGE_CURVE('',#2969,#2967,#1478,.T.);
#3856=EDGE_CURVE('',#2970,#2968,#1479,.T.);
#3857=EDGE_CURVE('',#2971,#2972,#1929,.T.);
#3858=EDGE_CURVE('',#2971,#2969,#1480,.T.);
#3859=EDGE_CURVE('',#2972,#2970,#1481,.T.);
#3860=EDGE_CURVE('',#2973,#2974,#1930,.T.);
#3861=EDGE_CURVE('',#2973,#2971,#1482,.T.);
#3862=EDGE_CURVE('',#2974,#2972,#1483,.T.);
#3863=EDGE_CURVE('',#2975,#2976,#1931,.T.);
#3864=EDGE_CURVE('',#2975,#2973,#1484,.T.);
#3865=EDGE_CURVE('',#2976,#2974,#1485,.T.);
#3866=EDGE_CURVE('',#2977,#2978,#1932,.T.);
#3867=EDGE_CURVE('',#2977,#2975,#1486,.T.);
#3868=EDGE_CURVE('',#2978,#2976,#1487,.T.);
#3869=EDGE_CURVE('',#2979,#2980,#1933,.T.);
#3870=EDGE_CURVE('',#2979,#2977,#1488,.T.);
#3871=EDGE_CURVE('',#2980,#2978,#1489,.T.);
#3872=EDGE_CURVE('',#2981,#2982,#1934,.T.);
#3873=EDGE_CURVE('',#2981,#2979,#1490,.T.);
#3874=EDGE_CURVE('',#2982,#2980,#1491,.T.);
#3875=EDGE_CURVE('',#2954,#2983,#1492,.T.);
#3876=EDGE_CURVE('',#2984,#2953,#1493,.T.);
#3877=EDGE_CURVE('',#2985,#2984,#1149,.T.);
#3878=EDGE_CURVE('',#2983,#2985,#1494,.T.);
#3879=EDGE_CURVE('',#2983,#2986,#1935,.T.);
#3880=EDGE_CURVE('',#2986,#2986,#1150,.T.);
#3881=EDGE_CURVE('',#2987,#2981,#1495,.T.);
#3882=EDGE_CURVE('',#2921,#2987,#1496,.T.);
#3883=EDGE_CURVE('',#2984,#2949,#1497,.T.);
#3884=EDGE_CURVE('',#2988,#2982,#1498,.T.);
#3885=EDGE_CURVE('',#2987,#2988,#1151,.T.);
#3886=EDGE_CURVE('',#2950,#2985,#1499,.T.);
#3887=EDGE_CURVE('',#2988,#2922,#1500,.T.);
#3888=EDGE_CURVE('',#2989,#2990,#1936,.T.);
#3889=EDGE_CURVE('',#2989,#2991,#1937,.T.);
#3890=EDGE_CURVE('',#2991,#2992,#1938,.T.);
#3891=EDGE_CURVE('',#2990,#2992,#1939,.T.);
#3892=EDGE_CURVE('',#2993,#2989,#1940,.T.);
#3893=EDGE_CURVE('',#2993,#2994,#1941,.T.);
#3894=EDGE_CURVE('',#2994,#2991,#1942,.T.);
#3895=EDGE_CURVE('',#2995,#2993,#1943,.T.);
#3896=EDGE_CURVE('',#2995,#2996,#1944,.T.);
#3897=EDGE_CURVE('',#2996,#2994,#1945,.T.);
#3898=EDGE_CURVE('',#2997,#2995,#1946,.T.);
#3899=EDGE_CURVE('',#2997,#2998,#1947,.T.);
#3900=EDGE_CURVE('',#2998,#2996,#1948,.T.);
#3901=EDGE_CURVE('',#2999,#2997,#1949,.T.);
#3902=EDGE_CURVE('',#2999,#3000,#1950,.T.);
#3903=EDGE_CURVE('',#3000,#2998,#1951,.T.);
#3904=EDGE_CURVE('',#2990,#2999,#1952,.T.);
#3905=EDGE_CURVE('',#2992,#3000,#1953,.T.);
#3906=EDGE_CURVE('',#3001,#3001,#1152,.T.);
#3907=EDGE_CURVE('',#3001,#3002,#1954,.T.);
#3908=EDGE_CURVE('',#3002,#3002,#1153,.T.);
#5447=ORIENTED_EDGE('',*,*,#3783,.F.);
#5448=ORIENTED_EDGE('',*,*,#3784,.T.);
#5449=ORIENTED_EDGE('',*,*,#3785,.T.);
#5450=ORIENTED_EDGE('',*,*,#3786,.T.);
#5451=ORIENTED_EDGE('',*,*,#3787,.F.);
#5452=ORIENTED_EDGE('',*,*,#3788,.T.);
#5453=ORIENTED_EDGE('',*,*,#3783,.T.);
#5454=ORIENTED_EDGE('',*,*,#3789,.T.);
#5455=ORIENTED_EDGE('',*,*,#3790,.F.);
#5456=ORIENTED_EDGE('',*,*,#3791,.T.);
#5457=ORIENTED_EDGE('',*,*,#3787,.T.);
#5458=ORIENTED_EDGE('',*,*,#3792,.T.);
#5459=ORIENTED_EDGE('',*,*,#3793,.F.);
#5460=ORIENTED_EDGE('',*,*,#3794,.T.);
#5461=ORIENTED_EDGE('',*,*,#3790,.T.);
#5462=ORIENTED_EDGE('',*,*,#3795,.T.);
#5463=ORIENTED_EDGE('',*,*,#3796,.F.);
#5464=ORIENTED_EDGE('',*,*,#3797,.T.);
#5465=ORIENTED_EDGE('',*,*,#3793,.T.);
#5466=ORIENTED_EDGE('',*,*,#3798,.T.);
#5467=ORIENTED_EDGE('',*,*,#3799,.F.);
#5468=ORIENTED_EDGE('',*,*,#3800,.T.);
#5469=ORIENTED_EDGE('',*,*,#3796,.T.);
#5470=ORIENTED_EDGE('',*,*,#3801,.T.);
#5471=ORIENTED_EDGE('',*,*,#3802,.F.);
#5472=ORIENTED_EDGE('',*,*,#3803,.T.);
#5473=ORIENTED_EDGE('',*,*,#3799,.T.);
#5474=ORIENTED_EDGE('',*,*,#3804,.T.);
#5475=ORIENTED_EDGE('',*,*,#3805,.F.);
#5476=ORIENTED_EDGE('',*,*,#3806,.T.);
#5477=ORIENTED_EDGE('',*,*,#3802,.T.);
#5478=ORIENTED_EDGE('',*,*,#3807,.T.);
#5479=ORIENTED_EDGE('',*,*,#3808,.F.);
#5480=ORIENTED_EDGE('',*,*,#3809,.T.);
#5481=ORIENTED_EDGE('',*,*,#3805,.T.);
#5482=ORIENTED_EDGE('',*,*,#3810,.T.);
#5483=ORIENTED_EDGE('',*,*,#3811,.F.);
#5484=ORIENTED_EDGE('',*,*,#3812,.T.);
#5485=ORIENTED_EDGE('',*,*,#3808,.T.);
#5486=ORIENTED_EDGE('',*,*,#3813,.T.);
#5487=ORIENTED_EDGE('',*,*,#3814,.F.);
#5488=ORIENTED_EDGE('',*,*,#3815,.T.);
#5489=ORIENTED_EDGE('',*,*,#3811,.T.);
#5490=ORIENTED_EDGE('',*,*,#3816,.T.);
#5491=ORIENTED_EDGE('',*,*,#3817,.F.);
#5492=ORIENTED_EDGE('',*,*,#3818,.T.);
#5493=ORIENTED_EDGE('',*,*,#3814,.T.);
#5494=ORIENTED_EDGE('',*,*,#3819,.T.);
#5495=ORIENTED_EDGE('',*,*,#3820,.F.);
#5496=ORIENTED_EDGE('',*,*,#3821,.T.);
#5497=ORIENTED_EDGE('',*,*,#3817,.T.);
#5498=ORIENTED_EDGE('',*,*,#3822,.T.);
#5499=ORIENTED_EDGE('',*,*,#3823,.F.);
#5500=ORIENTED_EDGE('',*,*,#3824,.T.);
#5501=ORIENTED_EDGE('',*,*,#3820,.T.);
#5502=ORIENTED_EDGE('',*,*,#3825,.T.);
#5503=ORIENTED_EDGE('',*,*,#3826,.F.);
#5504=ORIENTED_EDGE('',*,*,#3827,.T.);
#5505=ORIENTED_EDGE('',*,*,#3823,.T.);
#5506=ORIENTED_EDGE('',*,*,#3828,.T.);
#5507=ORIENTED_EDGE('',*,*,#3829,.F.);
#5508=ORIENTED_EDGE('',*,*,#3830,.T.);
#5509=ORIENTED_EDGE('',*,*,#3831,.T.);
#5510=ORIENTED_EDGE('',*,*,#3832,.F.);
#5511=ORIENTED_EDGE('',*,*,#3833,.F.);
#5512=ORIENTED_EDGE('',*,*,#3834,.T.);
#5513=ORIENTED_EDGE('',*,*,#3829,.T.);
#5514=ORIENTED_EDGE('',*,*,#3835,.F.);
#5515=ORIENTED_EDGE('',*,*,#3836,.F.);
#5516=ORIENTED_EDGE('',*,*,#3837,.T.);
#5517=ORIENTED_EDGE('',*,*,#3833,.T.);
#5518=ORIENTED_EDGE('',*,*,#3838,.F.);
#5519=ORIENTED_EDGE('',*,*,#3839,.F.);
#5520=ORIENTED_EDGE('',*,*,#3840,.T.);
#5521=ORIENTED_EDGE('',*,*,#3836,.T.);
#5522=ORIENTED_EDGE('',*,*,#3841,.F.);
#5523=ORIENTED_EDGE('',*,*,#3842,.F.);
#5524=ORIENTED_EDGE('',*,*,#3843,.T.);
#5525=ORIENTED_EDGE('',*,*,#3839,.T.);
#5526=ORIENTED_EDGE('',*,*,#3844,.F.);
#5527=ORIENTED_EDGE('',*,*,#3845,.F.);
#5528=ORIENTED_EDGE('',*,*,#3846,.T.);
#5529=ORIENTED_EDGE('',*,*,#3842,.T.);
#5530=ORIENTED_EDGE('',*,*,#3847,.F.);
#5531=ORIENTED_EDGE('',*,*,#3848,.F.);
#5532=ORIENTED_EDGE('',*,*,#3849,.T.);
#5533=ORIENTED_EDGE('',*,*,#3845,.T.);
#5534=ORIENTED_EDGE('',*,*,#3850,.F.);
#5535=ORIENTED_EDGE('',*,*,#3851,.F.);
#5536=ORIENTED_EDGE('',*,*,#3852,.T.);
#5537=ORIENTED_EDGE('',*,*,#3848,.T.);
#5538=ORIENTED_EDGE('',*,*,#3853,.F.);
#5539=ORIENTED_EDGE('',*,*,#3854,.F.);
#5540=ORIENTED_EDGE('',*,*,#3855,.T.);
#5541=ORIENTED_EDGE('',*,*,#3851,.T.);
#5542=ORIENTED_EDGE('',*,*,#3856,.F.);
#5543=ORIENTED_EDGE('',*,*,#3857,.F.);
#5544=ORIENTED_EDGE('',*,*,#3858,.T.);
#5545=ORIENTED_EDGE('',*,*,#3854,.T.);
#5546=ORIENTED_EDGE('',*,*,#3859,.F.);
#5547=ORIENTED_EDGE('',*,*,#3860,.F.);
#5548=ORIENTED_EDGE('',*,*,#3861,.T.);
#5549=ORIENTED_EDGE('',*,*,#3857,.T.);
#5550=ORIENTED_EDGE('',*,*,#3862,.F.);
#5551=ORIENTED_EDGE('',*,*,#3863,.F.);
#5552=ORIENTED_EDGE('',*,*,#3864,.T.);
#5553=ORIENTED_EDGE('',*,*,#3860,.T.);
#5554=ORIENTED_EDGE('',*,*,#3865,.F.);
#5555=ORIENTED_EDGE('',*,*,#3866,.F.);
#5556=ORIENTED_EDGE('',*,*,#3867,.T.);
#5557=ORIENTED_EDGE('',*,*,#3863,.T.);
#5558=ORIENTED_EDGE('',*,*,#3868,.F.);
#5559=ORIENTED_EDGE('',*,*,#3869,.F.);
#5560=ORIENTED_EDGE('',*,*,#3870,.T.);
#5561=ORIENTED_EDGE('',*,*,#3866,.T.);
#5562=ORIENTED_EDGE('',*,*,#3871,.F.);
#5563=ORIENTED_EDGE('',*,*,#3872,.F.);
#5564=ORIENTED_EDGE('',*,*,#3873,.T.);
#5565=ORIENTED_EDGE('',*,*,#3869,.T.);
#5566=ORIENTED_EDGE('',*,*,#3874,.F.);
#5567=ORIENTED_EDGE('',*,*,#3875,.F.);
#5568=ORIENTED_EDGE('',*,*,#3831,.F.);
#5569=ORIENTED_EDGE('',*,*,#3876,.F.);
#5570=ORIENTED_EDGE('',*,*,#3877,.F.);
#5571=ORIENTED_EDGE('',*,*,#3878,.F.);
#5572=ORIENTED_EDGE('',*,*,#3879,.T.);
#5573=ORIENTED_EDGE('',*,*,#3880,.F.);
#5574=ORIENTED_EDGE('',*,*,#3879,.F.);
#5575=ORIENTED_EDGE('',*,*,#3876,.T.);
#5576=ORIENTED_EDGE('',*,*,#3830,.F.);
#5577=ORIENTED_EDGE('',*,*,#3834,.F.);
#5578=ORIENTED_EDGE('',*,*,#3837,.F.);
#5579=ORIENTED_EDGE('',*,*,#3840,.F.);
#5580=ORIENTED_EDGE('',*,*,#3843,.F.);
#5581=ORIENTED_EDGE('',*,*,#3846,.F.);
#5582=ORIENTED_EDGE('',*,*,#3849,.F.);
#5583=ORIENTED_EDGE('',*,*,#3852,.F.);
#5584=ORIENTED_EDGE('',*,*,#3855,.F.);
#5585=ORIENTED_EDGE('',*,*,#3858,.F.);
#5586=ORIENTED_EDGE('',*,*,#3861,.F.);
#5587=ORIENTED_EDGE('',*,*,#3864,.F.);
#5588=ORIENTED_EDGE('',*,*,#3867,.F.);
#5589=ORIENTED_EDGE('',*,*,#3870,.F.);
#5590=ORIENTED_EDGE('',*,*,#3873,.F.);
#5591=ORIENTED_EDGE('',*,*,#3881,.F.);
#5592=ORIENTED_EDGE('',*,*,#3882,.F.);
#5593=ORIENTED_EDGE('',*,*,#3784,.F.);
#5594=ORIENTED_EDGE('',*,*,#3788,.F.);
#5595=ORIENTED_EDGE('',*,*,#3791,.F.);
#5596=ORIENTED_EDGE('',*,*,#3794,.F.);
#5597=ORIENTED_EDGE('',*,*,#3797,.F.);
#5598=ORIENTED_EDGE('',*,*,#3800,.F.);
#5599=ORIENTED_EDGE('',*,*,#3803,.F.);
#5600=ORIENTED_EDGE('',*,*,#3806,.F.);
#5601=ORIENTED_EDGE('',*,*,#3809,.F.);
#5602=ORIENTED_EDGE('',*,*,#3812,.F.);
#5603=ORIENTED_EDGE('',*,*,#3815,.F.);
#5604=ORIENTED_EDGE('',*,*,#3818,.F.);
#5605=ORIENTED_EDGE('',*,*,#3821,.F.);
#5606=ORIENTED_EDGE('',*,*,#3824,.F.);
#5607=ORIENTED_EDGE('',*,*,#3827,.F.);
#5608=ORIENTED_EDGE('',*,*,#3883,.F.);
#5609=ORIENTED_EDGE('',*,*,#3872,.T.);
#5610=ORIENTED_EDGE('',*,*,#3884,.F.);
#5611=ORIENTED_EDGE('',*,*,#3885,.F.);
#5612=ORIENTED_EDGE('',*,*,#3881,.T.);
#5613=ORIENTED_EDGE('',*,*,#3875,.T.);
#5614=ORIENTED_EDGE('',*,*,#3878,.T.);
#5615=ORIENTED_EDGE('',*,*,#3886,.F.);
#5616=ORIENTED_EDGE('',*,*,#3828,.F.);
#5617=ORIENTED_EDGE('',*,*,#3825,.F.);
#5618=ORIENTED_EDGE('',*,*,#3822,.F.);
#5619=ORIENTED_EDGE('',*,*,#3819,.F.);
#5620=ORIENTED_EDGE('',*,*,#3816,.F.);
#5621=ORIENTED_EDGE('',*,*,#3813,.F.);
#5622=ORIENTED_EDGE('',*,*,#3810,.F.);
#5623=ORIENTED_EDGE('',*,*,#3807,.F.);
#5624=ORIENTED_EDGE('',*,*,#3804,.F.);
#5625=ORIENTED_EDGE('',*,*,#3801,.F.);
#5626=ORIENTED_EDGE('',*,*,#3798,.F.);
#5627=ORIENTED_EDGE('',*,*,#3795,.F.);
#5628=ORIENTED_EDGE('',*,*,#3792,.F.);
#5629=ORIENTED_EDGE('',*,*,#3789,.F.);
#5630=ORIENTED_EDGE('',*,*,#3786,.F.);
#5631=ORIENTED_EDGE('',*,*,#3887,.F.);
#5632=ORIENTED_EDGE('',*,*,#3884,.T.);
#5633=ORIENTED_EDGE('',*,*,#3874,.T.);
#5634=ORIENTED_EDGE('',*,*,#3871,.T.);
#5635=ORIENTED_EDGE('',*,*,#3868,.T.);
#5636=ORIENTED_EDGE('',*,*,#3865,.T.);
#5637=ORIENTED_EDGE('',*,*,#3862,.T.);
#5638=ORIENTED_EDGE('',*,*,#3859,.T.);
#5639=ORIENTED_EDGE('',*,*,#3856,.T.);
#5640=ORIENTED_EDGE('',*,*,#3853,.T.);
#5641=ORIENTED_EDGE('',*,*,#3850,.T.);
#5642=ORIENTED_EDGE('',*,*,#3847,.T.);
#5643=ORIENTED_EDGE('',*,*,#3844,.T.);
#5644=ORIENTED_EDGE('',*,*,#3841,.T.);
#5645=ORIENTED_EDGE('',*,*,#3838,.T.);
#5646=ORIENTED_EDGE('',*,*,#3835,.T.);
#5647=ORIENTED_EDGE('',*,*,#3832,.T.);
#5648=ORIENTED_EDGE('',*,*,#3826,.T.);
#5649=ORIENTED_EDGE('',*,*,#3886,.T.);
#5650=ORIENTED_EDGE('',*,*,#3877,.T.);
#5651=ORIENTED_EDGE('',*,*,#3883,.T.);
#5652=ORIENTED_EDGE('',*,*,#3888,.F.);
#5653=ORIENTED_EDGE('',*,*,#3889,.T.);
#5654=ORIENTED_EDGE('',*,*,#3890,.T.);
#5655=ORIENTED_EDGE('',*,*,#3891,.F.);
#5656=ORIENTED_EDGE('',*,*,#3892,.F.);
#5657=ORIENTED_EDGE('',*,*,#3893,.T.);
#5658=ORIENTED_EDGE('',*,*,#3894,.T.);
#5659=ORIENTED_EDGE('',*,*,#3889,.F.);
#5660=ORIENTED_EDGE('',*,*,#3895,.F.);
#5661=ORIENTED_EDGE('',*,*,#3896,.T.);
#5662=ORIENTED_EDGE('',*,*,#3897,.T.);
#5663=ORIENTED_EDGE('',*,*,#3893,.F.);
#5664=ORIENTED_EDGE('',*,*,#3898,.F.);
#5665=ORIENTED_EDGE('',*,*,#3899,.T.);
#5666=ORIENTED_EDGE('',*,*,#3900,.T.);
#5667=ORIENTED_EDGE('',*,*,#3896,.F.);
#5668=ORIENTED_EDGE('',*,*,#3901,.F.);
#5669=ORIENTED_EDGE('',*,*,#3902,.T.);
#5670=ORIENTED_EDGE('',*,*,#3903,.T.);
#5671=ORIENTED_EDGE('',*,*,#3899,.F.);
#5672=ORIENTED_EDGE('',*,*,#3904,.F.);
#5673=ORIENTED_EDGE('',*,*,#3891,.T.);
#5674=ORIENTED_EDGE('',*,*,#3905,.T.);
#5675=ORIENTED_EDGE('',*,*,#3902,.F.);
#5676=ORIENTED_EDGE('',*,*,#3905,.F.);
#5677=ORIENTED_EDGE('',*,*,#3890,.F.);
#5678=ORIENTED_EDGE('',*,*,#3894,.F.);
#5679=ORIENTED_EDGE('',*,*,#3897,.F.);
#5680=ORIENTED_EDGE('',*,*,#3900,.F.);
#5681=ORIENTED_EDGE('',*,*,#3903,.F.);
#5682=ORIENTED_EDGE('',*,*,#3906,.T.);
#5683=ORIENTED_EDGE('',*,*,#3882,.T.);
#5684=ORIENTED_EDGE('',*,*,#3885,.T.);
#5685=ORIENTED_EDGE('',*,*,#3887,.T.);
#5686=ORIENTED_EDGE('',*,*,#3785,.F.);
#5687=ORIENTED_EDGE('',*,*,#3906,.F.);
#5688=ORIENTED_EDGE('',*,*,#3907,.T.);
#5689=ORIENTED_EDGE('',*,*,#3908,.T.);
#5690=ORIENTED_EDGE('',*,*,#3907,.F.);
#5691=ORIENTED_EDGE('',*,*,#3908,.F.);
#5692=ORIENTED_EDGE('',*,*,#3888,.T.);
#5693=ORIENTED_EDGE('',*,*,#3904,.T.);
#5694=ORIENTED_EDGE('',*,*,#3901,.T.);
#5695=ORIENTED_EDGE('',*,*,#3898,.T.);
#5696=ORIENTED_EDGE('',*,*,#3895,.T.);
#5697=ORIENTED_EDGE('',*,*,#3892,.T.);
#5698=ORIENTED_EDGE('',*,*,#3880,.T.);
#5988=CYLINDRICAL_SURFACE('',#6865,2.942);
#5989=CYLINDRICAL_SURFACE('',#6867,2.942);
#5990=CYLINDRICAL_SURFACE('',#6868,2.942);
#5991=CYLINDRICAL_SURFACE('',#6869,2.942);
#5992=CYLINDRICAL_SURFACE('',#6870,2.942);
#5993=CYLINDRICAL_SURFACE('',#6871,2.942);
#5994=CYLINDRICAL_SURFACE('',#6872,2.942);
#5995=CYLINDRICAL_SURFACE('',#6873,2.942);
#5996=CYLINDRICAL_SURFACE('',#6874,2.942);
#5997=CYLINDRICAL_SURFACE('',#6875,2.942);
#5998=CYLINDRICAL_SURFACE('',#6876,2.942);
#5999=CYLINDRICAL_SURFACE('',#6877,2.942);
#6000=CYLINDRICAL_SURFACE('',#6878,2.942);
#6001=CYLINDRICAL_SURFACE('',#6879,2.942);
#6002=CYLINDRICAL_SURFACE('',#6880,2.942);
#6003=CYLINDRICAL_SURFACE('',#6881,2.37175);
#6004=CYLINDRICAL_SURFACE('',#6883,2.37175);
#6005=CYLINDRICAL_SURFACE('',#6884,2.37175);
#6006=CYLINDRICAL_SURFACE('',#6885,2.37175);
#6007=CYLINDRICAL_SURFACE('',#6886,2.37175);
#6008=CYLINDRICAL_SURFACE('',#6887,2.37175);
#6009=CYLINDRICAL_SURFACE('',#6888,2.37175);
#6010=CYLINDRICAL_SURFACE('',#6889,2.37175);
#6011=CYLINDRICAL_SURFACE('',#6890,2.37175);
#6012=CYLINDRICAL_SURFACE('',#6891,2.37175);
#6013=CYLINDRICAL_SURFACE('',#6892,2.37175);
#6014=CYLINDRICAL_SURFACE('',#6893,2.37175);
#6015=CYLINDRICAL_SURFACE('',#6894,2.37175);
#6016=CYLINDRICAL_SURFACE('',#6895,2.37175);
#6017=CYLINDRICAL_SURFACE('',#6896,2.37175);
#6018=CYLINDRICAL_SURFACE('',#6900,2.37175);
#6019=CYLINDRICAL_SURFACE('',#6902,2.942);
#6020=CYLINDRICAL_SURFACE('',#6912,5.);
#6309=ADVANCED_FACE('',(#597),#5988,.T.);
#6310=ADVANCED_FACE('',(#598),#5989,.T.);
#6311=ADVANCED_FACE('',(#599),#5990,.T.);
#6312=ADVANCED_FACE('',(#600),#5991,.T.);
#6313=ADVANCED_FACE('',(#601),#5992,.T.);
#6314=ADVANCED_FACE('',(#602),#5993,.T.);
#6315=ADVANCED_FACE('',(#603),#5994,.T.);
#6316=ADVANCED_FACE('',(#604),#5995,.T.);
#6317=ADVANCED_FACE('',(#605),#5996,.T.);
#6318=ADVANCED_FACE('',(#606),#5997,.T.);
#6319=ADVANCED_FACE('',(#607),#5998,.T.);
#6320=ADVANCED_FACE('',(#608),#5999,.T.);
#6321=ADVANCED_FACE('',(#609),#6000,.T.);
#6322=ADVANCED_FACE('',(#610),#6001,.T.);
#6323=ADVANCED_FACE('',(#611),#6002,.T.);
#6324=ADVANCED_FACE('',(#612),#6003,.T.);
#6325=ADVANCED_FACE('',(#613),#6004,.T.);
#6326=ADVANCED_FACE('',(#614),#6005,.T.);
#6327=ADVANCED_FACE('',(#615),#6006,.T.);
#6328=ADVANCED_FACE('',(#616),#6007,.T.);
#6329=ADVANCED_FACE('',(#617),#6008,.T.);
#6330=ADVANCED_FACE('',(#618),#6009,.T.);
#6331=ADVANCED_FACE('',(#619),#6010,.T.);
#6332=ADVANCED_FACE('',(#620),#6011,.T.);
#6333=ADVANCED_FACE('',(#621),#6012,.T.);
#6334=ADVANCED_FACE('',(#622),#6013,.T.);
#6335=ADVANCED_FACE('',(#623),#6014,.T.);
#6336=ADVANCED_FACE('',(#624),#6015,.T.);
#6337=ADVANCED_FACE('',(#625),#6016,.T.);
#6338=ADVANCED_FACE('',(#626),#6017,.T.);
#6339=ADVANCED_FACE('',(#627),#80,.T.);
#6340=ADVANCED_FACE('',(#628),#139,.F.);
#6341=ADVANCED_FACE('',(#629),#6018,.T.);
#6342=ADVANCED_FACE('',(#630),#140,.F.);
#6343=ADVANCED_FACE('',(#631),#6019,.T.);
#6344=ADVANCED_FACE('',(#632),#293,.F.);
#6345=ADVANCED_FACE('',(#633),#294,.F.);
#6346=ADVANCED_FACE('',(#634),#295,.F.);
#6347=ADVANCED_FACE('',(#635),#296,.F.);
#6348=ADVANCED_FACE('',(#636),#297,.F.);
#6349=ADVANCED_FACE('',(#637),#298,.F.);
#6350=ADVANCED_FACE('',(#638),#299,.F.);
#6351=ADVANCED_FACE('',(#639,#191),#300,.T.);
#6352=ADVANCED_FACE('',(#640),#6020,.T.);
#6353=ADVANCED_FACE('',(#641,#192),#301,.F.);
#6354=ADVANCED_FACE('',(#642),#302,.T.);
#6388=CLOSED_SHELL('',(#6309,#6310,#6311,#6312,#6313,#6314,#6315,#6316,
#6317,#6318,#6319,#6320,#6321,#6322,#6323,#6324,#6325,#6326,#6327,#6328,
#6329,#6330,#6331,#6332,#6333,#6334,#6335,#6336,#6337,#6338,#6339,#6340,
#6341,#6342,#6343,#6344,#6345,#6346,#6347,#6348,#6349,#6350,#6351,#6352,
#6353,#6354));
#6864=AXIS2_PLACEMENT_3D('',#18205,#8067,#8068);
#6865=AXIS2_PLACEMENT_3D('',#18206,#8069,#8070);
#6866=AXIS2_PLACEMENT_3D('',#18222,#8072,#8073);
#6867=AXIS2_PLACEMENT_3D('',#18230,#8074,#8075);
#6868=AXIS2_PLACEMENT_3D('',#18278,#8077,#8078);
#6869=AXIS2_PLACEMENT_3D('',#18326,#8080,#8081);
#6870=AXIS2_PLACEMENT_3D('',#18380,#8083,#8084);
#6871=AXIS2_PLACEMENT_3D('',#18428,#8086,#8087);
#6872=AXIS2_PLACEMENT_3D('',#18476,#8089,#8090);
#6873=AXIS2_PLACEMENT_3D('',#18530,#8092,#8093);
#6874=AXIS2_PLACEMENT_3D('',#18578,#8095,#8096);
#6875=AXIS2_PLACEMENT_3D('',#18626,#8098,#8099);
#6876=AXIS2_PLACEMENT_3D('',#18680,#8101,#8102);
#6877=AXIS2_PLACEMENT_3D('',#18728,#8104,#8105);
#6878=AXIS2_PLACEMENT_3D('',#18776,#8107,#8108);
#6879=AXIS2_PLACEMENT_3D('',#18830,#8110,#8111);
#6880=AXIS2_PLACEMENT_3D('',#18878,#8113,#8114);
#6881=AXIS2_PLACEMENT_3D('',#18926,#8116,#8117);
#6882=AXIS2_PLACEMENT_3D('',#18942,#8119,#8120);
#6883=AXIS2_PLACEMENT_3D('',#18951,#8121,#8122);
#6884=AXIS2_PLACEMENT_3D('',#18976,#8124,#8125);
#6885=AXIS2_PLACEMENT_3D('',#19000,#8127,#8128);
#6886=AXIS2_PLACEMENT_3D('',#19025,#8130,#8131);
#6887=AXIS2_PLACEMENT_3D('',#19050,#8133,#8134);
#6888=AXIS2_PLACEMENT_3D('',#19074,#8136,#8137);
#6889=AXIS2_PLACEMENT_3D('',#19099,#8139,#8140);
#6890=AXIS2_PLACEMENT_3D('',#19124,#8142,#8143);
#6891=AXIS2_PLACEMENT_3D('',#19148,#8145,#8146);
#6892=AXIS2_PLACEMENT_3D('',#19173,#8148,#8149);
#6893=AXIS2_PLACEMENT_3D('',#19198,#8151,#8152);
#6894=AXIS2_PLACEMENT_3D('',#19222,#8154,#8155);
#6895=AXIS2_PLACEMENT_3D('',#19247,#8157,#8158);
#6896=AXIS2_PLACEMENT_3D('',#19272,#8160,#8161);
#6897=AXIS2_PLACEMENT_3D('',#19296,#8163,#8164);
#6898=AXIS2_PLACEMENT_3D('',#19584,#8165,#8166);
#6899=AXIS2_PLACEMENT_3D('',#19618,#8168,#8169);
#6900=AXIS2_PLACEMENT_3D('',#20143,#8170,#8171);
#6901=AXIS2_PLACEMENT_3D('',#20154,#8172,#8173);
#6902=AXIS2_PLACEMENT_3D('',#20681,#8174,#8175);
#6903=AXIS2_PLACEMENT_3D('',#20682,#8176,#8177);
#6904=AXIS2_PLACEMENT_3D('',#20691,#8182,#8183);
#6905=AXIS2_PLACEMENT_3D('',#20697,#8187,#8188);
#6906=AXIS2_PLACEMENT_3D('',#20703,#8192,#8193);
#6907=AXIS2_PLACEMENT_3D('',#20709,#8197,#8198);
#6908=AXIS2_PLACEMENT_3D('',#20715,#8202,#8203);
#6909=AXIS2_PLACEMENT_3D('',#20718,#8206,#8207);
#6910=AXIS2_PLACEMENT_3D('',#20719,#8208,#8209);
#6911=AXIS2_PLACEMENT_3D('',#20721,#8210,#8211);
#6912=AXIS2_PLACEMENT_3D('',#20722,#8212,#8213);
#6913=AXIS2_PLACEMENT_3D('',#20725,#8215,#8216);
#6914=AXIS2_PLACEMENT_3D('',#20726,#8217,#8218);
#6915=AXIS2_PLACEMENT_3D('',#20727,#8219,#8220);
#8067=DIRECTION('axis',(0.,0.,1.));
#8068=DIRECTION('refdir',(1.,0.,0.));
#8069=DIRECTION('center_axis',(0.,0.,1.));
#8070=DIRECTION('ref_axis',(1.,0.,0.));
#8071=DIRECTION('',(0.,0.,-1.));
#8072=DIRECTION('center_axis',(0.,0.,-1.));
#8073=DIRECTION('ref_axis',(1.,0.,0.));
#8074=DIRECTION('center_axis',(0.,0.,1.));
#8075=DIRECTION('ref_axis',(1.,0.,0.));
#8076=DIRECTION('',(0.,0.,-1.));
#8077=DIRECTION('center_axis',(0.,0.,1.));
#8078=DIRECTION('ref_axis',(1.,0.,0.));
#8079=DIRECTION('',(0.,0.,-1.));
#8080=DIRECTION('center_axis',(0.,0.,1.));
#8081=DIRECTION('ref_axis',(1.,0.,0.));
#8082=DIRECTION('',(0.,0.,-1.));
#8083=DIRECTION('center_axis',(0.,0.,1.));
#8084=DIRECTION('ref_axis',(1.,0.,0.));
#8085=DIRECTION('',(0.,0.,-1.));
#8086=DIRECTION('center_axis',(0.,0.,1.));
#8087=DIRECTION('ref_axis',(1.,0.,0.));
#8088=DIRECTION('',(0.,0.,-1.));
#8089=DIRECTION('center_axis',(0.,0.,1.));
#8090=DIRECTION('ref_axis',(1.,0.,0.));
#8091=DIRECTION('',(0.,0.,-1.));
#8092=DIRECTION('center_axis',(0.,0.,1.));
#8093=DIRECTION('ref_axis',(1.,0.,0.));
#8094=DIRECTION('',(0.,0.,-1.));
#8095=DIRECTION('center_axis',(0.,0.,1.));
#8096=DIRECTION('ref_axis',(1.,0.,0.));
#8097=DIRECTION('',(0.,0.,-1.));
#8098=DIRECTION('center_axis',(0.,0.,1.));
#8099=DIRECTION('ref_axis',(1.,0.,0.));
#8100=DIRECTION('',(0.,0.,-1.));
#8101=DIRECTION('center_axis',(0.,0.,1.));
#8102=DIRECTION('ref_axis',(1.,0.,0.));
#8103=DIRECTION('',(0.,0.,-1.));
#8104=DIRECTION('center_axis',(0.,0.,1.));
#8105=DIRECTION('ref_axis',(1.,0.,0.));
#8106=DIRECTION('',(0.,0.,-1.));
#8107=DIRECTION('center_axis',(0.,0.,1.));
#8108=DIRECTION('ref_axis',(1.,0.,0.));
#8109=DIRECTION('',(0.,0.,-1.));
#8110=DIRECTION('center_axis',(0.,0.,1.));
#8111=DIRECTION('ref_axis',(1.,0.,0.));
#8112=DIRECTION('',(0.,0.,-1.));
#8113=DIRECTION('center_axis',(0.,0.,1.));
#8114=DIRECTION('ref_axis',(1.,0.,0.));
#8115=DIRECTION('',(0.,0.,-1.));
#8116=DIRECTION('center_axis',(0.,0.,1.));
#8117=DIRECTION('ref_axis',(0.997339946684471,-0.0728905394918792,0.));
#8118=DIRECTION('',(0.,0.,1.));
#8119=DIRECTION('center_axis',(0.,0.,-1.));
#8120=DIRECTION('ref_axis',(1.,1.10476514494527E-13,0.));
#8121=DIRECTION('center_axis',(0.,0.,1.));
#8122=DIRECTION('ref_axis',(1.,1.10476514494527E-13,0.));
#8123=DIRECTION('',(0.,0.,1.));
#8124=DIRECTION('center_axis',(0.,0.,1.));
#8125=DIRECTION('ref_axis',(1.,1.10476514494527E-13,0.));
#8126=DIRECTION('',(0.,0.,1.));
#8127=DIRECTION('center_axis',(0.,0.,1.));
#8128=DIRECTION('ref_axis',(1.,1.10476514494527E-13,0.));
#8129=DIRECTION('',(0.,0.,1.));
#8130=DIRECTION('center_axis',(0.,0.,1.));
#8131=DIRECTION('ref_axis',(1.,1.10476514494527E-13,0.));
#8132=DIRECTION('',(0.,0.,1.));
#8133=DIRECTION('center_axis',(0.,0.,1.));
#8134=DIRECTION('ref_axis',(1.,1.10476514494527E-13,0.));
#8135=DIRECTION('',(0.,0.,1.));
#8136=DIRECTION('center_axis',(0.,0.,1.));
#8137=DIRECTION('ref_axis',(1.,1.10476514494527E-13,0.));
#8138=DIRECTION('',(0.,0.,1.));
#8139=DIRECTION('center_axis',(0.,0.,1.));
#8140=DIRECTION('ref_axis',(1.,1.10476514494527E-13,0.));
#8141=DIRECTION('',(0.,0.,1.));
#8142=DIRECTION('center_axis',(0.,0.,1.));
#8143=DIRECTION('ref_axis',(1.,1.10476514494527E-13,0.));
#8144=DIRECTION('',(0.,0.,1.));
#8145=DIRECTION('center_axis',(0.,0.,1.));
#8146=DIRECTION('ref_axis',(1.,1.10476514494527E-13,0.));
#8147=DIRECTION('',(0.,0.,1.));
#8148=DIRECTION('center_axis',(0.,0.,1.));
#8149=DIRECTION('ref_axis',(1.,1.10476514494527E-13,0.));
#8150=DIRECTION('',(0.,0.,1.));
#8151=DIRECTION('center_axis',(0.,0.,1.));
#8152=DIRECTION('ref_axis',(1.,1.10476514494527E-13,0.));
#8153=DIRECTION('',(0.,0.,1.));
#8154=DIRECTION('center_axis',(0.,0.,1.));
#8155=DIRECTION('ref_axis',(1.,1.10476514494527E-13,0.));
#8156=DIRECTION('',(0.,0.,1.));
#8157=DIRECTION('center_axis',(0.,0.,1.));
#8158=DIRECTION('ref_axis',(1.,1.10476514494527E-13,0.));
#8159=DIRECTION('',(0.,0.,1.));
#8160=DIRECTION('center_axis',(0.,0.,1.));
#8161=DIRECTION('ref_axis',(1.,1.10476514494527E-13,0.));
#8162=DIRECTION('',(0.,0.,1.));
#8163=DIRECTION('center_axis',(0.,0.,-1.));
#8164=DIRECTION('ref_axis',(1.,0.,0.));
#8165=DIRECTION('center_axis',(0.,0.,-1.));
#8166=DIRECTION('ref_axis',(1.,0.,0.));
#8167=DIRECTION('',(0.707106781186547,8.65956056235493E-17,0.707106781186548));
#8168=DIRECTION('center_axis',(0.,0.,1.));
#8169=DIRECTION('ref_axis',(1.,0.,0.));
#8170=DIRECTION('center_axis',(0.,0.,1.));
#8171=DIRECTION('ref_axis',(1.,1.10476514494527E-13,0.));
#8172=DIRECTION('center_axis',(0.,0.,-1.));
#8173=DIRECTION('ref_axis',(1.,1.10476514494527E-13,0.));
#8174=DIRECTION('center_axis',(0.,0.,1.));
#8175=DIRECTION('ref_axis',(1.,0.,0.));
#8176=DIRECTION('center_axis',(-1.92296268638356E-16,-1.,0.));
#8177=DIRECTION('ref_axis',(1.,-1.92296268638356E-16,0.));
#8178=DIRECTION('',(1.,-1.92296268638356E-16,0.));
#8179=DIRECTION('',(0.,0.,1.));
#8180=DIRECTION('',(1.,-1.92296268638356E-16,0.));
#8181=DIRECTION('',(0.,0.,1.));
#8182=DIRECTION('center_axis',(-0.866025403784439,-0.5,0.));
#8183=DIRECTION('ref_axis',(0.5,-0.866025403784439,0.));
#8184=DIRECTION('',(0.5,-0.866025403784439,0.));
#8185=DIRECTION('',(0.,0.,1.));
#8186=DIRECTION('',(0.5,-0.866025403784439,0.));
#8187=DIRECTION('center_axis',(-0.866025403784439,0.5,0.));
#8188=DIRECTION('ref_axis',(-0.5,-0.866025403784438,0.));
#8189=DIRECTION('',(-0.5,-0.866025403784438,0.));
#8190=DIRECTION('',(0.,0.,1.));
#8191=DIRECTION('',(-0.5,-0.866025403784439,0.));
#8192=DIRECTION('center_axis',(1.92296268638356E-16,1.,0.));
#8193=DIRECTION('ref_axis',(-1.,1.92296268638356E-16,0.));
#8194=DIRECTION('',(-1.,1.92296268638356E-16,0.));
#8195=DIRECTION('',(0.,0.,1.));
#8196=DIRECTION('',(-1.,1.92296268638356E-16,0.));
#8197=DIRECTION('center_axis',(0.866025403784439,0.5,0.));
#8198=DIRECTION('ref_axis',(-0.5,0.866025403784439,0.));
#8199=DIRECTION('',(-0.5,0.866025403784439,0.));
#8200=DIRECTION('',(0.,0.,1.));
#8201=DIRECTION('',(-0.5,0.866025403784439,0.));
#8202=DIRECTION('center_axis',(0.866025403784439,-0.5,0.));
#8203=DIRECTION('ref_axis',(0.5,0.866025403784439,0.));
#8204=DIRECTION('',(0.5,0.866025403784439,0.));
#8205=DIRECTION('',(0.5,0.866025403784439,0.));
#8206=DIRECTION('center_axis',(0.,0.,1.));
#8207=DIRECTION('ref_axis',(1.,0.,0.));
#8208=DIRECTION('center_axis',(0.,0.,1.));
#8209=DIRECTION('ref_axis',(1.,0.,0.));
#8210=DIRECTION('center_axis',(0.,0.,1.));
#8211=DIRECTION('ref_axis',(1.,0.,0.));
#8212=DIRECTION('center_axis',(0.,0.,1.));
#8213=DIRECTION('ref_axis',(1.,0.,0.));
#8214=DIRECTION('',(0.,0.,-1.));
#8215=DIRECTION('center_axis',(0.,0.,1.));
#8216=DIRECTION('ref_axis',(1.,0.,0.));
#8217=DIRECTION('center_axis',(0.,0.,1.));
#8218=DIRECTION('ref_axis',(1.,0.,0.));
#8219=DIRECTION('center_axis',(0.,0.,1.));
#8220=DIRECTION('ref_axis',(1.,0.,0.));
#18205=CARTESIAN_POINT('',(0.,0.,0.));
#18206=CARTESIAN_POINT('Origin',(0.,0.,0.));
#18207=CARTESIAN_POINT('',(-2.94490570994055,0.00214417779480537,0.322176117089595));
#18208=CARTESIAN_POINT('',(-2.94453111094736,0.00313617179185542,0.177823882910391));
#18209=CARTESIAN_POINT('',(-2.942,-3.60291088309151E-16,0.));
#18210=CARTESIAN_POINT('',(1.28892185405323,2.64462557919718,0.));
#18211=CARTESIAN_POINT('Ctrl Pts',(-2.94490570994055,0.00214417779480537,
0.322176117089595));
#18212=CARTESIAN_POINT('Ctrl Pts',(-2.94584715833611,0.124808428590093,
0.315520895872749));
#18213=CARTESIAN_POINT('Ctrl Pts',(-2.93884007386573,0.247358426874668,
0.308865674655903));
#18214=CARTESIAN_POINT('Ctrl Pts',(-2.92351947045398,0.368852411761562,
0.302210453439057));
#18215=CARTESIAN_POINT('Ctrl Pts',(-2.80238513102988,1.32946037267173,0.249590083068687));
#18216=CARTESIAN_POINT('Ctrl Pts',(-2.16153286152783,2.22405187279705,0.196969712698316));
#18217=CARTESIAN_POINT('Ctrl Pts',(-1.29099252632988,2.64857098947325,0.144349342327946));
#18218=CARTESIAN_POINT('Ctrl Pts',(-0.494964144347145,3.03675434170317,
0.0962328948852971));
#18219=CARTESIAN_POINT('Ctrl Pts',(0.493115753268411,3.03189109212113,0.0481164474426485));
#18220=CARTESIAN_POINT('Ctrl Pts',(1.29200104020318,2.64812001020929,-1.63834222883338E-16));
#18221=CARTESIAN_POINT('',(-1.28892185405328,2.64462557919715,0.));
#18222=CARTESIAN_POINT('Origin',(0.,0.,0.));
#18223=CARTESIAN_POINT('Ctrl Pts',(-1.28892185405328,2.64462557919715,2.08166817117217E-15));
#18224=CARTESIAN_POINT('Ctrl Pts',(-2.16403831185616,2.21811653527939,0.0526649636666859));
#18225=CARTESIAN_POINT('Ctrl Pts',(-2.80357657272064,1.32706756586464,0.10532992733337));
#18226=CARTESIAN_POINT('Ctrl Pts',(-2.92355402589586,0.366959843828546,
0.157994891000053));
#18227=CARTESIAN_POINT('Ctrl Pts',(-2.93861167702227,0.246462477535227,
0.164604554970166));
#18228=CARTESIAN_POINT('Ctrl Pts',(-2.94548559297357,0.124877349165528,
0.171214218940278));
#18229=CARTESIAN_POINT('Ctrl Pts',(-2.94453111094736,0.00313617179185542,
0.177823882910391));
#18230=CARTESIAN_POINT('Origin',(0.,0.,0.));
#18231=CARTESIAN_POINT('',(-2.93741501075088,0.000605053430647595,1.3221761170896));
#18232=CARTESIAN_POINT('',(-2.93743260967528,0.000720687897601403,1.17782388291039));
#18233=CARTESIAN_POINT('',(-2.942,-3.60291088309151E-16,0.));
#18234=CARTESIAN_POINT('Ctrl Pts',(-2.93741501075088,0.000605053430647595,
1.3221761170896));
#18235=CARTESIAN_POINT('Ctrl Pts',(-2.9382479568139,0.450815163107398,1.29790978476164));
#18236=CARTESIAN_POINT('Ctrl Pts',(-2.84099804532476,0.900683451883265,
1.27364345243368));
#18237=CARTESIAN_POINT('Ctrl Pts',(-2.64378204823906,1.30134356458571,1.24937712010572));
#18238=CARTESIAN_POINT('Ctrl Pts',(-2.21612867774369,2.17015567999336,1.19675674973535));
#18239=CARTESIAN_POINT('Ctrl Pts',(-1.31841648749453,2.80758195059898,1.14413637936498));
#18240=CARTESIAN_POINT('Ctrl Pts',(-0.357192829781819,2.92497002089294,
1.09151600899461));
#18241=CARTESIAN_POINT('Ctrl Pts',(0.604030827930888,3.04235809118689,1.03889563862424));
#18242=CARTESIAN_POINT('Ctrl Pts',(1.62876595310715,2.63970796116917,0.986275268253872));
#18243=CARTESIAN_POINT('Ctrl Pts',(2.25292793158662,1.89932766827126,0.933654897883501));
#18244=CARTESIAN_POINT('Ctrl Pts',(2.8770899100661,1.15894737537334,0.881034527513131));
#18245=CARTESIAN_POINT('Ctrl Pts',(3.1006787418488,0.0808369195952267,0.828414157142761));
#18246=CARTESIAN_POINT('Ctrl Pts',(2.82245137682484,-0.846673957408537,
0.775793786772391));
#18247=CARTESIAN_POINT('Ctrl Pts',(2.54422401180089,-1.7741848344123,0.72317341640202));
#18248=CARTESIAN_POINT('Ctrl Pts',(1.76418044997028,-2.55109613264171,0.67055304603165));
#18249=CARTESIAN_POINT('Ctrl Pts',(0.835554749603298,-2.82571794203434,
0.617932675661279));
#18250=CARTESIAN_POINT('Ctrl Pts',(-0.0930709507636752,-3.10033975142697,
0.565312305290909));
#18251=CARTESIAN_POINT('Ctrl Pts',(-1.17027878966702,-2.87267207198282,
0.512691934920538));
#18252=CARTESIAN_POINT('Ctrl Pts',(-1.90817450444562,-2.24552602141323,
0.460071564550168));
#18253=CARTESIAN_POINT('Ctrl Pts',(-2.55274401908064,-1.69769898118953,
0.414106415396644));
#18254=CARTESIAN_POINT('Ctrl Pts',(-2.93840347440061,-0.845052391620324,
0.368141266243119));
#18255=CARTESIAN_POINT('Ctrl Pts',(-2.94490570994055,0.00214417779480537,
0.322176117089595));
#18256=CARTESIAN_POINT('Ctrl Pts',(-2.94453111094736,0.00313617179185542,
0.177823882910391));
#18257=CARTESIAN_POINT('Ctrl Pts',(-2.93788040132423,-0.845140901703999,
0.223879182606963));
#18258=CARTESIAN_POINT('Ctrl Pts',(-2.55115114237882,-1.7009943502416,0.269934482303535));
#18259=CARTESIAN_POINT('Ctrl Pts',(-1.90455354763271,-2.24922658650796,
0.315989782000107));
#18260=CARTESIAN_POINT('Ctrl Pts',(-1.16515897070839,-2.87613882015091,
0.368654745666792));
#18261=CARTESIAN_POINT('Ctrl Pts',(-0.0859531713737992,-3.10079681277935,
0.421319709333476));
#18262=CARTESIAN_POINT('Ctrl Pts',(0.842833952810694,-2.82335342322726,
0.473984673000161));
#18263=CARTESIAN_POINT('Ctrl Pts',(1.77162107699519,-2.54591003367518,0.526649636666845));
#18264=CARTESIAN_POINT('Ctrl Pts',(2.54998952602959,-1.76636526194256,0.57931460033353));
#18265=CARTESIAN_POINT('Ctrl Pts',(2.82526196809064,-0.837265996441287,
0.631979564000215));
#18266=CARTESIAN_POINT('Ctrl Pts',(3.1005344101517,0.0918332690599885,0.684644527666899));
#18267=CARTESIAN_POINT('Ctrl Pts',(2.87271084523941,1.17048702832993,0.737309491333584));
#18268=CARTESIAN_POINT('Ctrl Pts',(2.2449320231631,1.90890163868963,0.789974455000268));
#18269=CARTESIAN_POINT('Ctrl Pts',(1.61715320108678,2.64731624904933,0.842639418666953));
#18270=CARTESIAN_POINT('Ctrl Pts',(0.589419121846451,3.0454917104988,0.895304382333637));
#18271=CARTESIAN_POINT('Ctrl Pts',(-0.37200976733393,2.9231058378395,0.947969346000322));
#18272=CARTESIAN_POINT('Ctrl Pts',(-1.33343865651431,2.8007199651802,1.00063430966701));
#18273=CARTESIAN_POINT('Ctrl Pts',(-2.22856235563474,2.15777275841214,1.05329927333369));
#18274=CARTESIAN_POINT('Ctrl Pts',(-2.6514251854394,1.28574400496261,1.10596423700038));
#18275=CARTESIAN_POINT('Ctrl Pts',(-2.8437527539192,0.889125626674557,1.12991745230371));
#18276=CARTESIAN_POINT('Ctrl Pts',(-2.93838674329414,0.445118617110292,
1.15387066760705));
#18277=CARTESIAN_POINT('Ctrl Pts',(-2.93743260967528,0.000720687897601403,
1.17782388291039));
#18278=CARTESIAN_POINT('Origin',(0.,0.,0.));
#18279=CARTESIAN_POINT('',(-2.94283216929169,-0.00254059509496668,2.3221761170896));
#18280=CARTESIAN_POINT('',(-2.94249560619114,-0.00258942729680482,2.17782388291039));
#18281=CARTESIAN_POINT('',(-2.942,-3.60291088309151E-16,0.));
#18282=CARTESIAN_POINT('Ctrl Pts',(-2.94283216929169,-0.00254059509496668,
2.3221761170896));
#18283=CARTESIAN_POINT('Ctrl Pts',(-2.93583836831966,0.770783310741536,
2.28029867365053));
#18284=CARTESIAN_POINT('Ctrl Pts',(-2.62244249954969,1.54912568223824,2.23842123021146));
#18285=CARTESIAN_POINT('Ctrl Pts',(-2.07534059520784,2.09189740289201,2.19654378677239));
#18286=CARTESIAN_POINT('Ctrl Pts',(-1.38788924974329,2.77390773164861,2.14392341640202));
#18287=CARTESIAN_POINT('Ctrl Pts',(-0.331445515483537,3.08398167899393,
2.09130304603165));
#18288=CARTESIAN_POINT('Ctrl Pts',(0.615553755286461,2.88169496582278,2.03868267566128));
#18289=CARTESIAN_POINT('Ctrl Pts',(1.56255302605646,2.67940825265162,1.98606230529091));
#18290=CARTESIAN_POINT('Ctrl Pts',(2.40010783333669,1.96476087896396,1.93344193492054));
#18291=CARTESIAN_POINT('Ctrl Pts',(2.74891040156469,1.06139789331815,1.88082156455017));
#18292=CARTESIAN_POINT('Ctrl Pts',(3.09771296979268,0.158034907672333,1.8282011941798));
#18293=CARTESIAN_POINT('Ctrl Pts',(2.95776329896845,-0.934043689931643,
1.77558082380943));
#18294=CARTESIAN_POINT('Ctrl Pts',(2.39244139669332,-1.72026117030417,1.72296045343906));
#18295=CARTESIAN_POINT('Ctrl Pts',(1.82711949441818,-2.50647865067671,1.67034008306869));
#18296=CARTESIAN_POINT('Ctrl Pts',(0.836425360692154,-2.9868350138178,1.61771971269832));
#18297=CARTESIAN_POINT('Ctrl Pts',(-0.130980997368149,-2.9437920444354,
1.56509934232795));
#18298=CARTESIAN_POINT('Ctrl Pts',(-1.09838735542844,-2.90074907505299,
1.51247897195758));
#18299=CARTESIAN_POINT('Ctrl Pts',(-2.04250593782301,-2.33430677314711,
1.45985860158721));
#18300=CARTESIAN_POINT('Ctrl Pts',(-2.5357679536495,-1.50098664208934,1.40723823121684));
#18301=CARTESIAN_POINT('Ctrl Pts',(-2.80155798635321,-1.05195919262036,
1.37888419317442));
#18302=CARTESIAN_POINT('Ctrl Pts',(-2.93644175348072,-0.525443729069001,
1.35053015513201));
#18303=CARTESIAN_POINT('Ctrl Pts',(-2.93741501075088,0.000605053430647595,
1.3221761170896));
#18304=CARTESIAN_POINT('Ctrl Pts',(-2.93743260967528,0.000720687897601403,
1.17782388291039));
#18305=CARTESIAN_POINT('Ctrl Pts',(-2.93628892837727,-0.53196109845813,
1.20653563127374));
#18306=CARTESIAN_POINT('Ctrl Pts',(-2.79780571115684,-1.06520455211536,
1.23524737963708));
#18307=CARTESIAN_POINT('Ctrl Pts',(-2.52560900690579,-1.51806949138664,
1.26395912800043));
#18308=CARTESIAN_POINT('Ctrl Pts',(-2.02632803807862,-2.34874393415536,
1.31662409166711));
#18309=CARTESIAN_POINT('Ctrl Pts',(-1.07716413993538,-2.9089825195618,1.3692890553338));
#18310=CARTESIAN_POINT('Ctrl Pts',(-0.108652539320438,-2.94471329972367,
1.42195401900048));
#18311=CARTESIAN_POINT('Ctrl Pts',(0.85985906129451,-2.98044407988555,1.47461898266717));
#18312=CARTESIAN_POINT('Ctrl Pts',(1.84771836438116,-2.49166705480286,1.52728394633385));
#18313=CARTESIAN_POINT('Ctrl Pts',(2.40686102399513,-1.70005997098112,1.57994891000054));
#18314=CARTESIAN_POINT('Ctrl Pts',(2.9660036836091,-0.908452887159384,1.63261387366722));
#18315=CARTESIAN_POINT('Ctrl Pts',(3.09642969975039,0.185984255401396,1.68527883733391));
#18316=CARTESIAN_POINT('Ctrl Pts',(2.73897659148843,1.08682694396802,1.73794380100059));
#18317=CARTESIAN_POINT('Ctrl Pts',(2.38152348322647,1.98766963253464,1.79060876466727));
#18318=CARTESIAN_POINT('Ctrl Pts',(1.53619125056127,2.69491786710711,1.84327372833396));
#18319=CARTESIAN_POINT('Ctrl Pts',(0.586406744725485,2.88778465426983,1.89593869200064));
#18320=CARTESIAN_POINT('Ctrl Pts',(-0.363377761110303,3.08065144143255,
1.94860365566733));
#18321=CARTESIAN_POINT('Ctrl Pts',(-1.41761454011667,2.75913678118554,2.00126861933401));
#18322=CARTESIAN_POINT('Ctrl Pts',(-2.09812527093809,2.0690698668059,2.0539335830007));
#18323=CARTESIAN_POINT('Ctrl Pts',(-2.63174175688638,1.52795998382732,2.09523034963726));
#18324=CARTESIAN_POINT('Ctrl Pts',(-2.93556254699721,0.76023565397735,2.13652711627383));
#18325=CARTESIAN_POINT('Ctrl Pts',(-2.94249560619114,-0.00258942729680482,
2.17782388291039));
#18326=CARTESIAN_POINT('Origin',(0.,0.,0.));
#18327=CARTESIAN_POINT('',(-2.94484294150901,0.00199174253909633,3.3221761170896));
#18328=CARTESIAN_POINT('',(-2.94526037616607,0.00180040430511289,3.17782388291039));
#18329=CARTESIAN_POINT('',(-2.942,-3.60291088309151E-16,0.));
#18330=CARTESIAN_POINT('Ctrl Pts',(-2.94484294150901,0.00199174253909633,
3.3221761170896));
#18331=CARTESIAN_POINT('Ctrl Pts',(-2.94583002736539,0.128597483532049,
3.31530793290979));
#18332=CARTESIAN_POINT('Ctrl Pts',(-2.93836342958051,0.255086036799256,
3.30843974872998));
#18333=CARTESIAN_POINT('Ctrl Pts',(-2.92204585589404,0.380422278131109,
3.30157156455017));
#18334=CARTESIAN_POINT('Ctrl Pts',(-2.79702929424561,1.34068182665933,3.2489511941798));
#18335=CARTESIAN_POINT('Ctrl Pts',(-2.15247739366928,2.23330287085301,3.19633082380943));
#18336=CARTESIAN_POINT('Ctrl Pts',(-1.28029158434589,2.65403966800756,3.14371045343906));
#18337=CARTESIAN_POINT('Ctrl Pts',(-0.4081057750225,3.0747764651621,3.09109008306869));
#18338=CARTESIAN_POINT('Ctrl Pts',(0.69171394304795,3.0236290152775,3.03846971269832));
#18339=CARTESIAN_POINT('Ctrl Pts',(1.5210867384019,2.5237607280468,2.98584934232795));
#18340=CARTESIAN_POINT('Ctrl Pts',(2.35045953375586,2.0238924408161,2.93322897195758));
#18341=CARTESIAN_POINT('Ctrl Pts',(2.90938540639331,1.07530331623929,2.8806086015872));
#18342=CARTESIAN_POINT('Ctrl Pts',(2.94474080948057,0.107585617606989,2.82798823121683));
#18343=CARTESIAN_POINT('Ctrl Pts',(2.98009621256783,-0.860132081025304,
2.77536786084646));
#18344=CARTESIAN_POINT('Ctrl Pts',(2.49188114610491,-1.84697835371309,2.7227474904761));
#18345=CARTESIAN_POINT('Ctrl Pts',(1.70119600494326,-2.40603518007504,2.67012712010573));
#18346=CARTESIAN_POINT('Ctrl Pts',(0.91051086378161,-2.965092006437,2.61750674973535));
#18347=CARTESIAN_POINT('Ctrl Pts',(-0.182644352078765,-3.09635938647313,
2.56488637936498));
#18348=CARTESIAN_POINT('Ctrl Pts',(-1.08320700768761,-2.74038967310636,
2.51226600899461));
#18349=CARTESIAN_POINT('Ctrl Pts',(-1.98376966329644,-2.3844199597396,2.45964563862424));
#18350=CARTESIAN_POINT('Ctrl Pts',(-2.69173975865374,-1.54121315296996,
2.40702526825387));
#18351=CARTESIAN_POINT('Ctrl Pts',(-2.88649532799773,-0.59263639450121,
2.3544048978835));
#18352=CARTESIAN_POINT('Ctrl Pts',(-2.92625644781122,-0.398975826678611,
2.3436619709522));
#18353=CARTESIAN_POINT('Ctrl Pts',(-2.94462630681883,-0.200923340849699,
2.3329190440209));
#18354=CARTESIAN_POINT('Ctrl Pts',(-2.94283216929169,-0.00254059509496668,
2.3221761170896));
#18355=CARTESIAN_POINT('Ctrl Pts',(-2.94249560619114,-0.00258942729680482,
2.17782388291039));
#18356=CARTESIAN_POINT('Ctrl Pts',(-2.94440414260591,-0.212580342560449,
2.18919207994051));
#18357=CARTESIAN_POINT('Ctrl Pts',(-2.92381470891138,-0.422199995772688,
2.20056027697063));
#18358=CARTESIAN_POINT('Ctrl Pts',(-2.87932772554241,-0.626618874207943,
2.21192847400075));
#18359=CARTESIAN_POINT('Ctrl Pts',(-2.67323476668884,-1.57362153232989,
2.26459343766743));
#18360=CARTESIAN_POINT('Ctrl Pts',(-1.95426416634525,-2.40900768006153,
2.31725840133412));
#18361=CARTESIAN_POINT('Ctrl Pts',(-1.04852602468143,-2.75386472764491,
2.3699233650008));
#18362=CARTESIAN_POINT('Ctrl Pts',(-0.142787883017607,-3.09872177522829,
2.42258832866749));
#18363=CARTESIAN_POINT('Ctrl Pts',(0.949717799966449,-2.95304972266342,
2.47525329233417));
#18364=CARTESIAN_POINT('Ctrl Pts',(1.7334537997702,-2.38292188563198,2.52791825600086));
#18365=CARTESIAN_POINT('Ctrl Pts',(2.51718979957395,-1.81279404860055,2.58058321966754));
#18366=CARTESIAN_POINT('Ctrl Pts',(2.99215611619739,-0.818210427102559,
2.63324818333423));
#18367=CARTESIAN_POINT('Ctrl Pts',(2.94291803037279,0.149706737509724,2.68591314700091));
#18368=CARTESIAN_POINT('Ctrl Pts',(2.89367994454819,1.11762390212201,2.7385781106676));
#18369=CARTESIAN_POINT('Ctrl Pts',(2.32023745627556,2.05887460984858,2.79124307433428));
#18370=CARTESIAN_POINT('Ctrl Pts',(1.4826919461771,2.54652764310569,2.84390803800096));
#18371=CARTESIAN_POINT('Ctrl Pts',(0.645146436078633,3.03418067636279,2.89657300166765));
#18372=CARTESIAN_POINT('Ctrl Pts',(-0.456502095845658,3.06823603515044,
2.94923796533433));
#18373=CARTESIAN_POINT('Ctrl Pts',(-1.32256928803916,2.63324686948073,3.00190292900102));
#18374=CARTESIAN_POINT('Ctrl Pts',(-2.18863648023266,2.19825770381101,3.0545678926677));
#18375=CARTESIAN_POINT('Ctrl Pts',(-2.81912233269536,1.29422401368392,3.10723285633439));
#18376=CARTESIAN_POINT('Ctrl Pts',(-2.92805183726137,0.331196319314338,
3.15989782000107));
#18377=CARTESIAN_POINT('Ctrl Pts',(-2.94041095304778,0.221931425219236,
3.16587317430418));
#18378=CARTESIAN_POINT('Ctrl Pts',(-2.94605601250203,0.111907094355046,
3.17184852860728));
#18379=CARTESIAN_POINT('Ctrl Pts',(-2.94526037616607,0.00180040430511289,
3.17782388291039));
#18380=CARTESIAN_POINT('Origin',(0.,0.,0.));
#18381=CARTESIAN_POINT('',(-2.93739242931988,0.000540407572186541,4.3221761170896));
#18382=CARTESIAN_POINT('',(-2.93753500859377,0.000882026442511373,4.17782388291039));
#18383=CARTESIAN_POINT('',(-2.942,-3.60291088309151E-16,0.));
#18384=CARTESIAN_POINT('Ctrl Pts',(-2.93739242931988,0.000540407572186541,
4.3221761170896));
#18385=CARTESIAN_POINT('Ctrl Pts',(-2.93814630501522,0.454709257120266,
4.29769682179868));
#18386=CARTESIAN_POINT('Ctrl Pts',(-2.83910536028106,0.908566671316128,
4.27321752650776));
#18387=CARTESIAN_POINT('Ctrl Pts',(-2.6385374625564,1.31194251096478,4.24873823121684));
#18388=CARTESIAN_POINT('Ctrl Pts',(-2.20739935432037,2.17903389691023,4.19611786084646));
#18389=CARTESIAN_POINT('Ctrl Pts',(-1.30713327152341,2.8128638865229,4.14349749047609));
#18390=CARTESIAN_POINT('Ctrl Pts',(-0.345447198709921,2.92638673563265,
4.09087712010572));
#18391=CARTESIAN_POINT('Ctrl Pts',(0.616238874103564,3.0399095847424,4.03825674973536));
#18392=CARTESIAN_POINT('Ctrl Pts',(1.63934493693357,2.63312529334921,3.98563637936499));
#18393=CARTESIAN_POINT('Ctrl Pts',(2.26053185174972,1.89025628960273,3.93301600899462));
#18394=CARTESIAN_POINT('Ctrl Pts',(2.88171876656588,1.14738728585625,3.88039563862425));
#18395=CARTESIAN_POINT('Ctrl Pts',(3.10098653336818,0.0684335697564567,
3.82777526825387));
#18396=CARTESIAN_POINT('Ctrl Pts',(2.8190342665149,-0.857973716122647,3.7751548978835));
#18397=CARTESIAN_POINT('Ctrl Pts',(2.53708199966161,-1.78438100200175,3.72253452751313));
#18398=CARTESIAN_POINT('Ctrl Pts',(1.75390969915275,-2.55824185766015,3.66991415714276));
#18399=CARTESIAN_POINT('Ctrl Pts',(0.824196505293748,-2.82909406262337,
3.61729378677239));
#18400=CARTESIAN_POINT('Ctrl Pts',(-0.105516688565254,-3.09994626758658,
3.56467341640202));
#18401=CARTESIAN_POINT('Ctrl Pts',(-1.18177077577439,-2.86778982185459,
3.51205304603165));
#18402=CARTESIAN_POINT('Ctrl Pts',(-1.91715720801869,-2.23776257255722,
3.45943267566128));
#18403=CARTESIAN_POINT('Ctrl Pts',(-2.55655857926025,-1.68996855643583,
3.41368048947072));
#18404=CARTESIAN_POINT('Ctrl Pts',(-2.93826750108625,-0.841388295482023,
3.36792830328016));
#18405=CARTESIAN_POINT('Ctrl Pts',(-2.94484294150901,0.00199174253909633,
3.3221761170896));
#18406=CARTESIAN_POINT('Ctrl Pts',(-2.94526037616607,0.00180040430511289,
3.17782388291039));
#18407=CARTESIAN_POINT('Ctrl Pts',(-2.93904351473207,-0.858539934689441,
3.22451349227397));
#18408=CARTESIAN_POINT('Ctrl Pts',(-2.53959728591596,-1.72390862024193,
3.27120310163755));
#18409=CARTESIAN_POINT('Ctrl Pts',(-1.87733008879233,-2.27130145042432,
3.31789271100113));
#18410=CARTESIAN_POINT('Ctrl Pts',(-1.13030567908798,-2.88874982718133,
3.37055767466781));
#18411=CARTESIAN_POINT('Ctrl Pts',(-0.0488837030099704,-3.10162488208327,
3.4232226383345));
#18412=CARTESIAN_POINT('Ctrl Pts',(0.876425794829888,-2.81337100100799,
3.47588760200118));
#18413=CARTESIAN_POINT('Ctrl Pts',(1.80173529266975,-2.5251171199327,3.52855256566786));
#18414=CARTESIAN_POINT('Ctrl Pts',(2.57093231227146,-1.73573430288019,3.58121752933455));
#18415=CARTESIAN_POINT('Ctrl Pts',(2.83512541526138,-0.803269840348294,
3.63388249300123));
#18416=CARTESIAN_POINT('Ctrl Pts',(3.0993185182513,0.129194622183599,3.68654745666792));
#18417=CARTESIAN_POINT('Ctrl Pts',(2.85850770462944,1.20474073019488,3.7392124203346));
#18418=CARTESIAN_POINT('Ctrl Pts',(2.22191964750238,1.93552360728328,3.79187738400129));
#18419=CARTESIAN_POINT('Ctrl Pts',(1.58533159037532,2.66630648437168,3.84454234766797));
#18420=CARTESIAN_POINT('Ctrl Pts',(0.552966289743035,3.05232613053722,3.89720731133465));
#18421=CARTESIAN_POINT('Ctrl Pts',(-0.406917273431679,2.91849222887777,
3.94987227500134));
#18422=CARTESIAN_POINT('Ctrl Pts',(-1.36680083660641,2.78465832721833,4.00253723866802));
#18423=CARTESIAN_POINT('Ctrl Pts',(-2.25420266232356,2.13097087773392,4.05520220233471));
#18424=CARTESIAN_POINT('Ctrl Pts',(-2.666616123304,1.25392862924115,4.10786716600139));
#18425=CARTESIAN_POINT('Ctrl Pts',(-2.84922387445754,0.865593310885713,
4.13118607163773));
#18426=CARTESIAN_POINT('Ctrl Pts',(-2.9387088904313,0.433468688742346,4.15450497727406));
#18427=CARTESIAN_POINT('Ctrl Pts',(-2.93753500859377,0.000882026442511374,
4.17782388291039));
#18428=CARTESIAN_POINT('Origin',(0.,0.,0.));
#18429=CARTESIAN_POINT('',(-2.94294893056736,-0.00252441656932667,5.3221761170896));
#18430=CARTESIAN_POINT('',(-2.94214529852914,-0.00261326515612426,5.1778238829104));
#18431=CARTESIAN_POINT('',(-2.942,-3.60291088309151E-16,0.));
#18432=CARTESIAN_POINT('Ctrl Pts',(-2.94294893056736,-0.00252441656932667,
5.3221761170896));
#18433=CARTESIAN_POINT('Ctrl Pts',(-2.93593381851913,0.774652637504292,
5.28008571068756));
#18434=CARTESIAN_POINT('Ctrl Pts',(-2.61899610205614,1.55689120032164,5.23799530428553));
#18435=CARTESIAN_POINT('Ctrl Pts',(-2.06692649506365,2.10021140779169,5.1959048978835));
#18436=CARTESIAN_POINT('Ctrl Pts',(-1.37674291943613,2.77945670358908,5.14328452751313));
#18437=CARTESIAN_POINT('Ctrl Pts',(-0.31906293568821,3.08528758407071,5.09066415714276));
#18438=CARTESIAN_POINT('Ctrl Pts',(0.627116654359043,2.8792008952563,5.03804378677239));
#18439=CARTESIAN_POINT('Ctrl Pts',(1.5732962444063,2.67311420644189,4.98542341640202));
#18440=CARTESIAN_POINT('Ctrl Pts',(2.4079754407529,1.95510994833143,4.93280304603165));
#18441=CARTESIAN_POINT('Ctrl Pts',(2.75314891878373,1.05035428518759,4.88018267566128));
#18442=CARTESIAN_POINT('Ctrl Pts',(3.09832239681456,0.145598622043775,4.82756230529091));
#18443=CARTESIAN_POINT('Ctrl Pts',(2.95399015652965,-0.945908446133409,
4.77494193492054));
#18444=CARTESIAN_POINT('Ctrl Pts',(2.38551665840565,-1.72985067733577,4.72232156455017));
#18445=CARTESIAN_POINT('Ctrl Pts',(1.81704316028163,-2.51379290853814,4.6697011941798));
#18446=CARTESIAN_POINT('Ctrl Pts',(0.824428404318513,-2.99017030276568,
4.61708082380943));
#18447=CARTESIAN_POINT('Ctrl Pts',(-0.142797221412707,-2.9432434569701,
4.56446045343906));
#18448=CARTESIAN_POINT('Ctrl Pts',(-1.11002284714393,-2.89631661117452,
4.51184008306869));
#18449=CARTESIAN_POINT('Ctrl Pts',(-2.05185934264326,-2.32608552535581,
4.45921971269832));
#18450=CARTESIAN_POINT('Ctrl Pts',(-2.54177252355539,-1.49079359130735,
4.40659934232795));
#18451=CARTESIAN_POINT('Ctrl Pts',(-2.80377530896762,-1.04408421119714,
4.3784582672485));
#18452=CARTESIAN_POINT('Ctrl Pts',(-2.93652578376122,-0.52156611314212,
4.35031719216905));
#18453=CARTESIAN_POINT('Ctrl Pts',(-2.93739242931988,0.000540407572186541,
4.3221761170896));
#18454=CARTESIAN_POINT('Ctrl Pts',(-2.93753500859377,0.000882026442511374,
4.17782388291039));
#18455=CARTESIAN_POINT('Ctrl Pts',(-2.93605771780397,-0.543513730930775,
4.20716994094074));
#18456=CARTESIAN_POINT('Ctrl Pts',(-2.79100052624987,-1.08864123864977,
4.23651599897109));
#18457=CARTESIAN_POINT('Ctrl Pts',(-2.50727405993036,-1.54814577624058,
4.26586205700145));
#18458=CARTESIAN_POINT('Ctrl Pts',(-1.99809343933257,-2.37278088572845,
4.31852702066813));
#18459=CARTESIAN_POINT('Ctrl Pts',(-1.04230710189327,-2.92165405720309,
4.37119198433482));
#18460=CARTESIAN_POINT('Ctrl Pts',(-0.0734394371752462,-2.94580807344744,
4.4238569480015));
#18461=CARTESIAN_POINT('Ctrl Pts',(0.895428227542791,-2.9699620896918,4.47652191166818));
#18462=CARTESIAN_POINT('Ctrl Pts',(1.87737721953956,-2.46939695070584,4.52918687533487));
#18463=CARTESIAN_POINT('Ctrl Pts',(2.427016324523,-1.67115837574717,4.58185183900155));
#18464=CARTESIAN_POINT('Ctrl Pts',(2.97665542950643,-0.872919800788501,
4.63451680266824));
#18465=CARTESIAN_POINT('Ctrl Pts',(3.09398464747655,0.22299221014288,4.68718176633492));
#18466=CARTESIAN_POINT('Ctrl Pts',(2.725785936287,1.11949523708763,4.73984673000161));
#18467=CARTESIAN_POINT('Ctrl Pts',(2.35758722509745,2.01599826403239,4.79251169366829));
#18468=CARTESIAN_POINT('Ctrl Pts',(1.50386058474821,2.71309230699052,4.84517665733498));
#18469=CARTESIAN_POINT('Ctrl Pts',(0.551838293166775,2.8945903085884,4.89784162100166));
#18470=CARTESIAN_POINT('Ctrl Pts',(-0.400183998414646,3.07608831018627,
4.95050658466835));
#18471=CARTESIAN_POINT('Ctrl Pts',(-1.45050194122825,2.74199027042391,5.00317154833503));
#18472=CARTESIAN_POINT('Ctrl Pts',(-2.12271361651498,2.04383596665945,5.05583651200172));
#18473=CARTESIAN_POINT('Ctrl Pts',(-2.64172618991724,1.50479316935294,5.09649896897128));
#18474=CARTESIAN_POINT('Ctrl Pts',(-2.93533688440644,0.748724173372516,
5.13716142594084));
#18475=CARTESIAN_POINT('Ctrl Pts',(-2.94214529852914,-0.00261326515612426,
5.1778238829104));
#18476=CARTESIAN_POINT('Origin',(0.,0.,0.));
#18477=CARTESIAN_POINT('',(-2.94474230559933,0.0020353165097306,6.3221761170896));
#18478=CARTESIAN_POINT('',(-2.94552589459255,0.00164462538419303,6.1778238829104));
#18479=CARTESIAN_POINT('',(-2.942,-3.60291088309151E-16,0.));
#18480=CARTESIAN_POINT('Ctrl Pts',(-2.94474230559933,0.0020353165097306,
6.3221761170896));
#18481=CARTESIAN_POINT('Ctrl Pts',(-2.94577608567865,0.132578411608025,
6.31509496994683));
#18482=CARTESIAN_POINT('Ctrl Pts',(-2.93783733482844,0.262995037552802,
6.30801382280405));
#18483=CARTESIAN_POINT('Ctrl Pts',(-2.92049520368276,0.39214902611321,6.30093267566128));
#18484=CARTESIAN_POINT('Ctrl Pts',(-2.79162493090094,1.35189898976081,6.24831230529091));
#18485=CARTESIAN_POINT('Ctrl Pts',(-2.1434950231737,2.24192544902223,6.19569193492054));
#18486=CARTESIAN_POINT('Ctrl Pts',(-1.26962729970534,2.65915768867859,6.14307156455017));
#18487=CARTESIAN_POINT('Ctrl Pts',(-0.395759576236975,3.07638992833495,
6.0904511941798));
#18488=CARTESIAN_POINT('Ctrl Pts',(0.70384596297251,3.02082794838624,6.03783082380943));
#18489=CARTESIAN_POINT('Ctrl Pts',(1.53120548099802,2.51763437940803,5.98521045343906));
#18490=CARTESIAN_POINT('Ctrl Pts',(2.35856499902354,2.0144408104298,5.93259008306869));
#18491=CARTESIAN_POINT('Ctrl Pts',(2.91367849586509,1.06361565242206,5.87996971269832));
#18492=CARTESIAN_POINT('Ctrl Pts',(2.9451489575673,0.0957638301017936,5.82734934232795));
#18493=CARTESIAN_POINT('Ctrl Pts',(2.97661941926951,-0.872087992218468,
5.77472897195758));
#18494=CARTESIAN_POINT('Ctrl Pts',(2.48444684583239,-1.85696647885126,5.72210860158721));
#18495=CARTESIAN_POINT('Ctrl Pts',(1.69152388176343,-2.41284480454905,5.66948823121684));
#18496=CARTESIAN_POINT('Ctrl Pts',(0.898600917694462,-2.96872313024685,
5.61686786084646));
#18497=CARTESIAN_POINT('Ctrl Pts',(-0.19507243700635,-3.09560129500965,
5.56424749047609));
#18498=CARTESIAN_POINT('Ctrl Pts',(-1.09419888335647,-2.73601935246765,
5.51162712010572));
#18499=CARTESIAN_POINT('Ctrl Pts',(-1.9933253297066,-2.37643740992565,5.45900674973535));
#18500=CARTESIAN_POINT('Ctrl Pts',(-2.69790486770603,-1.53039536007885,
5.40638637936499));
#18501=CARTESIAN_POINT('Ctrl Pts',(-2.88885105295217,-0.581044479598858,
5.35376600899461));
#18502=CARTESIAN_POINT('Ctrl Pts',(-2.92706166295704,-0.391068040923041,
5.34323604502627));
#18503=CARTESIAN_POINT('Ctrl Pts',(-2.94470393564848,-0.196954622309047,
5.33270608105794));
#18504=CARTESIAN_POINT('Ctrl Pts',(-2.94294893056736,-0.00252441656932667,
5.3221761170896));
#18505=CARTESIAN_POINT('Ctrl Pts',(-2.94214529852914,-0.00261326515612426,
5.1778238829104));
#18506=CARTESIAN_POINT('Ctrl Pts',(-2.94415496646843,-0.224388664623296,
5.18982638960752));
#18507=CARTESIAN_POINT('Ctrl Pts',(-2.92117618657372,-0.445751813963285,
5.20182889630465));
#18508=CARTESIAN_POINT('Ctrl Pts',(-2.87162987121487,-0.660999575716158,
5.21383140300177));
#18509=CARTESIAN_POINT('Ctrl Pts',(-2.65422904286817,-1.60547024656074,
5.26649636666845));
#18510=CARTESIAN_POINT('Ctrl Pts',(-1.92532197841492,-2.43220102048334,
5.31916133033513));
#18511=CARTESIAN_POINT('Ctrl Pts',(-1.01552544630456,-2.76620437138433,
5.37182629400182));
#18512=CARTESIAN_POINT('Ctrl Pts',(-0.105728914194198,-3.10020772228531,
5.4244912576685));
#18513=CARTESIAN_POINT('Ctrl Pts',(0.984957085573281,-2.94148365016469,
5.47715622133519));
#18514=CARTESIAN_POINT('Ctrl Pts',(1.761820540694,-2.36202602414577,5.52982118500188));
#18515=CARTESIAN_POINT('Ctrl Pts',(2.53868399581473,-1.78256839812686,5.58248614866856));
#18516=CARTESIAN_POINT('Ctrl Pts',(3.0017249062887,-0.782377218209647,5.63515111233524));
#18517=CARTESIAN_POINT('Ctrl Pts',(2.94091774630216,0.184882032222853,5.68781607600193));
#18518=CARTESIAN_POINT('Ctrl Pts',(2.88011058631563,1.15214128265535,5.74048103966861));
#18519=CARTESIAN_POINT('Ctrl Pts',(2.2954553558686,2.08646860360313,5.7931460033353));
#18520=CARTESIAN_POINT('Ctrl Pts',(1.45213925422783,2.56407295970403,5.84581096700198));
#18521=CARTESIAN_POINT('Ctrl Pts',(0.60882315258705,3.04167731580494,5.89847593066867));
#18522=CARTESIAN_POINT('Ctrl Pts',(-0.493153820247473,3.06255870705896,
5.95114089433535));
#18523=CARTESIAN_POINT('Ctrl Pts',(-1.35395830631657,2.6172457777424,6.00380585800203));
#18524=CARTESIAN_POINT('Ctrl Pts',(-2.21476279238567,2.17193284842583,6.05647082166872));
#18525=CARTESIAN_POINT('Ctrl Pts',(-2.83439479168936,1.26042559853868,6.10913578533541));
#18526=CARTESIAN_POINT('Ctrl Pts',(-2.93180238522596,0.296164363719765,
6.16180074900209));
#18527=CARTESIAN_POINT('Ctrl Pts',(-2.94168102690256,0.198373309905978,
6.1671417936382));
#18528=CARTESIAN_POINT('Ctrl Pts',(-2.94618853440423,0.100039675683843,
6.1724828382743));
#18529=CARTESIAN_POINT('Ctrl Pts',(-2.94552589459255,0.00164462538419303,
6.1778238829104));
#18530=CARTESIAN_POINT('Origin',(0.,0.,0.));
#18531=CARTESIAN_POINT('',(-2.93737184280031,0.000478285809368539,7.32217611708959));
#18532=CARTESIAN_POINT('',(-2.93765213932985,0.00105817779144944,7.17782388291039));
#18533=CARTESIAN_POINT('',(-2.942,-3.60291088309151E-16,0.));
#18534=CARTESIAN_POINT('Ctrl Pts',(-2.93737184280031,0.000478285809368539,
7.32217611708959));
#18535=CARTESIAN_POINT('Ctrl Pts',(-2.93804459091945,0.458606303769958,
7.29748385883571));
#18536=CARTESIAN_POINT('Ctrl Pts',(-2.83719423177179,0.916453996322869,
7.27279160058183));
#18537=CARTESIAN_POINT('Ctrl Pts',(-2.63324974290992,1.32252368027208,7.24809934232795));
#18538=CARTESIAN_POINT('Ctrl Pts',(-2.198634389848,2.18787738530332,7.19547897195758));
#18539=CARTESIAN_POINT('Ctrl Pts',(-1.29583121079705,2.81808837804428,7.14285860158721));
#18540=CARTESIAN_POINT('Ctrl Pts',(-0.333697177699206,2.92774986756231,
7.09023823121684));
#18541=CARTESIAN_POINT('Ctrl Pts',(0.628436855398639,3.03741135708034,7.03761786084647));
#18542=CARTESIAN_POINT('Ctrl Pts',(1.64990174254338,2.62652334337548,6.9849974904761));
#18543=CARTESIAN_POINT('Ctrl Pts',(2.26810159307568,1.88116672756646,6.93237712010573));
#18544=CARTESIAN_POINT('Ctrl Pts',(2.886301443608,1.13581011175742,6.87975674973536));
#18545=CARTESIAN_POINT('Ctrl Pts',(3.10123625752784,0.055984893844227,6.82713637936498));
#18546=CARTESIAN_POINT('Ctrl Pts',(2.81556743521199,-0.869283101865742,
6.77451600899461));
#18547=CARTESIAN_POINT('Ctrl Pts',(2.52989861289615,-1.7945510975757,6.72189563862424));
#18548=CARTESIAN_POINT('Ctrl Pts',(1.74362615434463,-2.56526187108243,6.66927526825387));
#18549=CARTESIAN_POINT('Ctrl Pts',(0.812833183747132,-2.8323797960046,6.6166548978835));
#18550=CARTESIAN_POINT('Ctrl Pts',(-0.117959786850361,-3.09949772092676,
6.56403452751313));
#18551=CARTESIAN_POINT('Ctrl Pts',(-1.19327326949384,-2.86302279726437,
6.51141415714276));
#18552=CARTESIAN_POINT('Ctrl Pts',(-1.92612469189739,-2.23004860141629,
6.45879378677239));
#18553=CARTESIAN_POINT('Ctrl Pts',(-2.56035596550109,-1.68225403062272,
6.41325456354479));
#18554=CARTESIAN_POINT('Ctrl Pts',(-2.93809401248361,-0.83749407451141,
6.3677153403172));
#18555=CARTESIAN_POINT('Ctrl Pts',(-2.94474230559933,0.0020353165097306,
6.3221761170896));
#18556=CARTESIAN_POINT('Ctrl Pts',(-2.94552589459255,0.00164462538419303,
6.1778238829104));
#18557=CARTESIAN_POINT('Ctrl Pts',(-2.93965462503178,-0.87017722046166,
6.22514780194098));
#18558=CARTESIAN_POINT('Ctrl Pts',(-2.52789003171806,-1.74682066505967,
6.27247172097156));
#18559=CARTESIAN_POINT('Ctrl Pts',(-1.85003983495055,-2.2935847848838,6.31979564000214));
#18560=CARTESIAN_POINT('Ctrl Pts',(-1.095686503369,-2.90205747891776,6.37246060366883));
#18561=CARTESIAN_POINT('Ctrl Pts',(-0.0117966524363787,-3.10198764723502,
6.42512556733551));
#18562=CARTESIAN_POINT('Ctrl Pts',(0.910000294361383,-2.80269121035772,
6.4777905310022));
#18563=CARTESIAN_POINT('Ctrl Pts',(1.83179724115916,-2.50339477348041,6.53045549466888));
#18564=CARTESIAN_POINT('Ctrl Pts',(2.59150128382206,-1.70487173140855,6.58312045833556));
#18565=CARTESIAN_POINT('Ctrl Pts',(2.8445267984577,-0.769315181970455,6.63578542200225));
#18566=CARTESIAN_POINT('Ctrl Pts',(3.09755231309333,0.166241367467632,6.68845038566893));
#18567=CARTESIAN_POINT('Ctrl Pts',(2.84389929970168,1.23883142427194,6.74111534933562));
#18568=CARTESIAN_POINT('Ctrl Pts',(2.19861937965545,1.96195091165853,6.79378031300231));
#18569=CARTESIAN_POINT('Ctrl Pts',(1.55333945960922,2.68507039904512,6.84644527666899));
#18570=CARTESIAN_POINT('Ctrl Pts',(0.51643263290838,3.05871931701401,6.89911024033567));
#18571=CARTESIAN_POINT('Ctrl Pts',(-0.441782179220013,2.91341844960141,
6.95177520400236));
#18572=CARTESIAN_POINT('Ctrl Pts',(-1.39999699134843,2.76811758218879,7.00444016766904));
#18573=CARTESIAN_POINT('Ctrl Pts',(-2.2795197889044,2.10386692939468,7.05710513133573));
#18574=CARTESIAN_POINT('Ctrl Pts',(-2.68141770473996,1.22195648411116,7.10977009500241));
#18575=CARTESIAN_POINT('Ctrl Pts',(-2.85452884366231,0.842087578115104,
7.13245469097174));
#18576=CARTESIAN_POINT('Ctrl Pts',(-2.93902534565796,0.421835844039577,
7.15513928694107));
#18577=CARTESIAN_POINT('Ctrl Pts',(-2.93765213932985,0.00105817779144944,
7.17782388291039));
#18578=CARTESIAN_POINT('Origin',(0.,0.,0.));
#18579=CARTESIAN_POINT('',(-2.94306537549688,-0.00250657139928612,8.3221761170896));
#18580=CARTESIAN_POINT('',(-2.94179645842688,-0.00262223567938445,8.17782388291039));
#18581=CARTESIAN_POINT('',(-2.942,-3.60291088309151E-16,0.));
#18582=CARTESIAN_POINT('Ctrl Pts',(-2.94306537549688,-0.00250657139928612,
8.3221761170896));
#18583=CARTESIAN_POINT('Ctrl Pts',(-2.93603346312234,0.778523040326291,
8.2798727477246));
#18584=CARTESIAN_POINT('Ctrl Pts',(-2.6155295502631,1.5646541741046,8.23756937835961));
#18585=CARTESIAN_POINT('Ctrl Pts',(-2.0584790752992,2.10849163858216,8.19526600899462));
#18586=CARTESIAN_POINT('Ctrl Pts',(-1.36557440251332,2.78496089461673,8.14264563862425));
#18587=CARTESIAN_POINT('Ctrl Pts',(-0.306675260078988,3.08654352280986,
8.09002526825387));
#18588=CARTESIAN_POINT('Ctrl Pts',(0.638669423716989,2.87666029635488,8.0374048978835));
#18589=CARTESIAN_POINT('Ctrl Pts',(1.58401410751295,2.66677706989991,7.98478452751313));
#18590=CARTESIAN_POINT('Ctrl Pts',(2.41580433267058,1.94542798879682,7.93216415714276));
#18591=CARTESIAN_POINT('Ctrl Pts',(2.75734311734437,1.03929400395132,7.87954378677239));
#18592=CARTESIAN_POINT('Ctrl Pts',(3.09888190201817,0.133160019105817,7.82692341640202));
#18593=CARTESIAN_POINT('Ctrl Pts',(2.95016924620815,-0.957758869482093,
7.77430304603165));
#18594=CARTESIAN_POINT('Ctrl Pts',(2.37855339098706,-1.73941279161662,7.72168267566128));
#18595=CARTESIAN_POINT('Ctrl Pts',(1.80693753576595,-2.52106671375116,7.66906230529091));
#18596=CARTESIAN_POINT('Ctrl Pts',(0.812418481133763,-2.99345566943229,
7.61644193492054));
#18597=CARTESIAN_POINT('Ctrl Pts',(-0.154610975618871,-2.94264651965433,
7.56382156455017));
#18598=CARTESIAN_POINT('Ctrl Pts',(-1.1216404323715,-2.89183736987637,7.5112011941798));
#18599=CARTESIAN_POINT('Ctrl Pts',(-2.06118029124457,-2.31783011463932,
7.45858082380943));
#18600=CARTESIAN_POINT('Ctrl Pts',(-2.54773645714466,-1.48057827836003,
7.40596045343906));
#18601=CARTESIAN_POINT('Ctrl Pts',(-2.80597476023112,-1.03620924430037,
7.37803234132257));
#18602=CARTESIAN_POINT('Ctrl Pts',(-2.93661093285418,-0.517686173583286,
7.35010422920608));
#18603=CARTESIAN_POINT('Ctrl Pts',(-2.93737184280031,0.000478285809368539,
7.32217611708959));
#18604=CARTESIAN_POINT('Ctrl Pts',(-2.93765213932985,0.00105817779144944,
7.17782388291039));
#18605=CARTESIAN_POINT('Ctrl Pts',(-2.93583728528984,-0.555049110608679,
7.20780425060775));
#18606=CARTESIAN_POINT('Ctrl Pts',(-2.78403605908896,-1.11207503097007,
7.23778461830511));
#18607=CARTESIAN_POINT('Ctrl Pts',(-2.48858495099342,-1.57801251517323,
7.26776498600247));
#18608=CARTESIAN_POINT('Ctrl Pts',(-1.96958124729618,-2.39650083140119,
7.32042994966915));
#18609=CARTESIAN_POINT('Ctrl Pts',(-1.00730080578659,-2.93390722608419,
7.37309491333584));
#18610=CARTESIAN_POINT('Ctrl Pts',(-0.0382136038189444,-2.94647556868157,
7.42575987700252));
#18611=CARTESIAN_POINT('Ctrl Pts',(0.930873598148709,-2.95904391127895,
7.47842484066921));
#18612=CARTESIAN_POINT('Ctrl Pts',(1.90676756057442,-2.44677420179069,7.53108980433588));
#18613=CARTESIAN_POINT('Ctrl Pts',(2.44682350205541,-1.64202110404938,7.58375476800257));
#18614=CARTESIAN_POINT('Ctrl Pts',(2.98687944353639,-0.837268006308086,
7.63641973166925));
#18615=CARTESIAN_POINT('Ctrl Pts',(3.09109736407267,0.25996847968624,7.68908469533594));
#18616=CARTESIAN_POINT('Ctrl Pts',(2.71220622763963,1.15200518015635,7.74174965900263));
#18617=CARTESIAN_POINT('Ctrl Pts',(2.33331509120659,2.04404188062646,7.79441462266931));
#18618=CARTESIAN_POINT('Ctrl Pts',(1.47131489780423,2.73087879557235,7.84707958633599));
#18619=CARTESIAN_POINT('Ctrl Pts',(0.517190633372317,2.90098128313613,7.89974455000268));
#18620=CARTESIAN_POINT('Ctrl Pts',(-0.436933631059594,3.07108377069992,
7.95240951366936));
#18621=CARTESIAN_POINT('Ctrl Pts',(-1.48318196652107,2.72445183088159,8.00507447733605));
#18622=CARTESIAN_POINT('Ctrl Pts',(-2.14699834174799,2.01831035197405,8.05773944100273));
#18623=CARTESIAN_POINT('Ctrl Pts',(-2.65153376339188,1.48160562142403,8.09776758830529));
#18624=CARTESIAN_POINT('Ctrl Pts',(-2.93514585523751,0.737219387421443,
8.13779573560784));
#18625=CARTESIAN_POINT('Ctrl Pts',(-2.94179645842688,-0.00262223567938445,
8.17782388291039));
#18626=CARTESIAN_POINT('Origin',(0.,0.,0.));
#18627=CARTESIAN_POINT('',(-2.94464008512449,0.00207742171232136,9.3221761170896));
#18628=CARTESIAN_POINT('',(-2.94577110767244,0.00147777103002609,9.1778238829104));
#18629=CARTESIAN_POINT('',(-2.942,-3.60291088309151E-16,0.));
#18630=CARTESIAN_POINT('Ctrl Pts',(-2.94464008512449,0.00207742171232136,
9.3221761170896));
#18631=CARTESIAN_POINT('Ctrl Pts',(-2.94572064417758,0.136558752036829,
9.31488200698387));
#18632=CARTESIAN_POINT('Ctrl Pts',(-2.93729508396668,0.270903986837675,
9.30758789687813));
#18633=CARTESIAN_POINT('Ctrl Pts',(-2.91889749004766,0.4038694541666,9.3002937867724));
#18634=CARTESIAN_POINT('Ctrl Pts',(-2.7861755826581,1.3630943679524,9.24767341640203));
#18635=CARTESIAN_POINT('Ctrl Pts',(-2.1344781113937,2.25051190295123,9.19505304603165));
#18636=CARTESIAN_POINT('Ctrl Pts',(-1.25894255572533,2.66423286046833,9.14243267566128));
#18637=CARTESIAN_POINT('Ctrl Pts',(-0.383407000056953,3.07795381798544,
9.08981230529091));
#18638=CARTESIAN_POINT('Ctrl Pts',(0.715966640015389,3.01797819802083,9.03719193492054));
#18639=CARTESIAN_POINT('Ctrl Pts',(1.54129954888374,2.51146745828537,8.98457156455017));
#18640=CARTESIAN_POINT('Ctrl Pts',(2.3666324577521,2.00495671854991,8.9319511941798));
#18641=CARTESIAN_POINT('Ctrl Pts',(2.91792463541645,1.05191085904358,8.87933082380943));
#18642=CARTESIAN_POINT('Ctrl Pts',(2.94550964776859,0.0839405046308018,
8.82671045343906));
#18643=CARTESIAN_POINT('Ctrl Pts',(2.97309466012074,-0.884029849781979,
8.77409008306869));
#18644=CARTESIAN_POINT('Ctrl Pts',(2.47697250716068,-1.86692469910122,8.72146971269832));
#18645=CARTESIAN_POINT('Ctrl Pts',(1.68182449914462,-2.41961555778857,8.66884934232795));
#18646=CARTESIAN_POINT('Ctrl Pts',(0.886676491128584,-2.97230641647591,
8.61622897195757));
#18647=CARTESIAN_POINT('Ctrl Pts',(-0.207497371943416,-3.09479328453138,
8.56360860158721));
#18648=CARTESIAN_POINT('Ctrl Pts',(-1.10517312337017,-2.73160492399537,
8.51098823121684));
#18649=CARTESIAN_POINT('Ctrl Pts',(-2.00284887479693,-2.36841656345936,
8.45836786084647));
#18650=CARTESIAN_POINT('Ctrl Pts',(-2.70402651457844,-1.51955297433185,
8.4057474904761));
#18651=CARTESIAN_POINT('Ctrl Pts',(-2.89116023290047,-0.56944323783011,
8.35312712010573));
#18652=CARTESIAN_POINT('Ctrl Pts',(-2.92785056302318,-0.383160187412328,
8.34281011910035));
#18653=CARTESIAN_POINT('Ctrl Pts',(-2.94478032747652,-0.192985093804385,
8.33249311809497));
#18654=CARTESIAN_POINT('Ctrl Pts',(-2.94306537549688,-0.00250657139928612,
8.3221761170896));
#18655=CARTESIAN_POINT('Ctrl Pts',(-2.94179645842688,-0.00262223567938445,
8.17782388291039));
#18656=CARTESIAN_POINT('Ctrl Pts',(-2.94389604226671,-0.236188947098698,
8.19046069927452));
#18657=CARTESIAN_POINT('Ctrl Pts',(-2.91839215134056,-0.469302718100354,
8.20309751563865));
#18658=CARTESIAN_POINT('Ctrl Pts',(-2.86352159037298,-0.695286025907358,
8.21573433200279));
#18659=CARTESIAN_POINT('Ctrl Pts',(-2.63484404877868,-1.63708990688444,
8.26839929566947));
#18660=CARTESIAN_POINT('Ctrl Pts',(-1.89610455059774,-2.45504665084187,
8.32106425933616));
#18661=CARTESIAN_POINT('Ctrl Pts',(-0.982379647459882,-2.77814844538783,
8.37372922300284));
#18662=CARTESIAN_POINT('Ctrl Pts',(-0.068654744322021,-3.1012502399338,
8.42639418666953));
#18663=CARTESIAN_POINT('Ctrl Pts',(1.02005556377276,-2.92949708506828,8.47905915033621));
#18664=CARTESIAN_POINT('Ctrl Pts',(1.78993539631662,-2.34079256521527,8.53172411400289));
#18665=CARTESIAN_POINT('Ctrl Pts',(2.55981522886048,-1.75208804536226,8.58438907766958));
#18666=CARTESIAN_POINT('Ctrl Pts',(3.01086458585342,-0.746432160521719,
8.63705404133626));
#18667=CARTESIAN_POINT('Ctrl Pts',(2.93849705553841,0.220030931794408,8.68971900500295));
#18668=CARTESIAN_POINT('Ctrl Pts',(2.86612952522341,1.18649402411053,8.74238396866963));
#18669=CARTESIAN_POINT('Ctrl Pts',(2.27034510760049,2.11376432390223,8.79504893233632));
#18670=CARTESIAN_POINT('Ctrl Pts',(1.42137896494728,2.58125171077128,8.847713896003));
#18671=CARTESIAN_POINT('Ctrl Pts',(0.572412822294062,3.04873909764032,8.90037885966968));
#18672=CARTESIAN_POINT('Ctrl Pts',(-0.529735045389435,3.05644357158669,
8.95304382333637));
#18673=CARTESIAN_POINT('Ctrl Pts',(-1.38515376586909,2.60087054680792,9.00570878700305));
#18674=CARTESIAN_POINT('Ctrl Pts',(-2.24057248634875,2.14529752202914,9.05837375066974));
#18675=CARTESIAN_POINT('Ctrl Pts',(-2.84926205962455,1.2264469985252,9.11103871433643));
#18676=CARTESIAN_POINT('Ctrl Pts',(-2.93513381881397,0.261090064936974,
9.16370367800311));
#18677=CARTESIAN_POINT('Ctrl Pts',(-2.94280828744918,0.174814884615283,
9.16841041297221));
#18678=CARTESIAN_POINT('Ctrl Pts',(-2.94630689264378,0.0881682471389342,
9.1731171479413));
#18679=CARTESIAN_POINT('Ctrl Pts',(-2.94577110767244,0.00147777103002609,
9.1778238829104));
#18680=CARTESIAN_POINT('Origin',(0.,0.,0.));
#18681=CARTESIAN_POINT('',(-2.93735377875815,0.0004158914717875,10.3221761170896));
#18682=CARTESIAN_POINT('',(-2.93779053274574,0.00122895754932335,10.1778238829104));
#18683=CARTESIAN_POINT('',(-2.942,-3.60291088309151E-16,0.));
#18684=CARTESIAN_POINT('Ctrl Pts',(-2.93735377875815,0.0004158914717875,
10.3221761170896));
#18685=CARTESIAN_POINT('Ctrl Pts',(-2.93794360094505,0.462502223744089,
10.2972708958728));
#18686=CARTESIAN_POINT('Ctrl Pts',(-2.83526550161259,0.924340675123848,
10.2723656746559));
#18687=CARTESIAN_POINT('Ctrl Pts',(-2.6279195904465,1.33308353810155,10.2474604534391));
#18688=CARTESIAN_POINT('Ctrl Pts',(-2.18983399605069,2.19668561771623,10.1948400830687));
#18689=CARTESIAN_POINT('Ctrl Pts',(-1.28450826872579,2.82326745826868,10.1422197126983));
#18690=CARTESIAN_POINT('Ctrl Pts',(-0.321941779407734,2.9290658210569,10.0895993423279));
#18691=CARTESIAN_POINT('Ctrl Pts',(0.640624709910309,3.03486418384512,10.0369789719576));
#18692=CARTESIAN_POINT('Ctrl Pts',(1.66043196122149,2.61987906886913,9.98435860158721));
#18693=CARTESIAN_POINT('Ctrl Pts',(2.27563478565877,1.87204685190273,9.93173823121684));
#18694=CARTESIAN_POINT('Ctrl Pts',(2.89083761009605,1.12421463493634,9.87911786084647));
#18695=CARTESIAN_POINT('Ctrl Pts',(3.10143600765941,0.0435353159795382,
9.82649749047609));
#18696=CARTESIAN_POINT('Ctrl Pts',(2.8120552331994,-0.880578479665677,9.77387712010572));
#18697=CARTESIAN_POINT('Ctrl Pts',(2.52267445873939,-1.8046922753109,9.72125674973535));
#18698=CARTESIAN_POINT('Ctrl Pts',(1.733314512256,-2.57224054764455,9.66863637936499));
#18699=CARTESIAN_POINT('Ctrl Pts',(0.801456763974427,-2.83561988794246,
9.61601600899462));
#18700=CARTESIAN_POINT('Ctrl Pts',(-0.130400984307143,-3.09899922824038,
9.56339563862425));
#18701=CARTESIAN_POINT('Ctrl Pts',(-1.20475653438691,-2.85820963650256,
9.51077526825387));
#18702=CARTESIAN_POINT('Ctrl Pts',(-1.93506113766943,-2.22229869434726,
9.4581548978835));
#18703=CARTESIAN_POINT('Ctrl Pts',(-2.5641326605009,-1.67453620870937,9.41282863761886));
#18704=CARTESIAN_POINT('Ctrl Pts',(-2.93792539338528,-0.833601734574448,
9.36750237735423));
#18705=CARTESIAN_POINT('Ctrl Pts',(-2.94464008512449,0.00207742171232136,
9.3221761170896));
#18706=CARTESIAN_POINT('Ctrl Pts',(-2.94577110767244,0.00147777103002609,
9.1778238829104));
#18707=CARTESIAN_POINT('Ctrl Pts',(-2.94031184592155,-0.881835546255158,
9.22578211160798));
#18708=CARTESIAN_POINT('Ctrl Pts',(-2.51599664630944,-1.76970025068938,
9.27374034030557));
#18709=CARTESIAN_POINT('Ctrl Pts',(-1.82248510748737,-2.31554023703778,
9.32169856900316));
#18710=CARTESIAN_POINT('Ctrl Pts',(-1.06091069186834,-2.91495026175178,
9.37436353266984));
#18711=CARTESIAN_POINT('Ctrl Pts',(0.0252920844727601,-3.1019069675073,
9.42702849633653));
#18712=CARTESIAN_POINT('Ctrl Pts',(0.943444704192239,-2.79161076199491,
9.47969346000322));
#18713=CARTESIAN_POINT('Ctrl Pts',(1.86159732391172,-2.48131455648253,9.5323584236699));
#18714=CARTESIAN_POINT('Ctrl Pts',(2.61169978700958,-1.67376543970224,9.58502338733658));
#18715=CARTESIAN_POINT('Ctrl Pts',(2.85352154222556,-0.735250545330611,
9.63768835100327));
#18716=CARTESIAN_POINT('Ctrl Pts',(3.09534329744155,0.203264349041017,9.69035331466995));
#18717=CARTESIAN_POINT('Ctrl Pts',(2.82888434477565,1.27274502100399,9.74301827833664));
#18718=CARTESIAN_POINT('Ctrl Pts',(2.17500480776272,1.98809774472063,9.79568324200333));
#18719=CARTESIAN_POINT('Ctrl Pts',(1.52112527074978,2.70345046843728,9.84834820567001));
#18720=CARTESIAN_POINT('Ctrl Pts',(0.479825149389799,3.06467524390761,9.90101316933669));
#18721=CARTESIAN_POINT('Ctrl Pts',(-0.476583929910364,2.90792818241875,
9.95367813300337));
#18722=CARTESIAN_POINT('Ctrl Pts',(-1.43299300921054,2.75118112092989,10.0063430966701));
#18723=CARTESIAN_POINT('Ctrl Pts',(-2.3045110464509,2.07646222248183,10.0590080603367));
#18724=CARTESIAN_POINT('Ctrl Pts',(-2.69583596380714,1.18980965393578,10.1116730240034));
#18725=CARTESIAN_POINT('Ctrl Pts',(-2.85967973895049,0.818577213506006,
10.1337233103058));
#18726=CARTESIAN_POINT('Ctrl Pts',(-2.93934508420187,0.410192546500391,
10.1557735966081));
#18727=CARTESIAN_POINT('Ctrl Pts',(-2.93779053274574,0.00122895754932335,
10.1778238829104));
#18728=CARTESIAN_POINT('Origin',(0.,0.,0.));
#18729=CARTESIAN_POINT('',(-2.94318142996902,-0.00248705772575741,11.3221761170896));
#18730=CARTESIAN_POINT('',(-2.94145083142593,-0.00261642954227547,11.1778238829104));
#18731=CARTESIAN_POINT('',(-2.942,-3.60291088309151E-16,0.));
#18732=CARTESIAN_POINT('Ctrl Pts',(-2.94318142996902,-0.00248705772575741,
11.3221761170896));
#18733=CARTESIAN_POINT('Ctrl Pts',(-2.93613735245544,0.782394524444463,
11.2796597847616));
#18734=CARTESIAN_POINT('Ctrl Pts',(-2.61204283140731,1.57241444895454,11.2371434524337));
#18735=CARTESIAN_POINT('Ctrl Pts',(-2.04999848462302,2.11673789269853,11.1946271201057));
#18736=CARTESIAN_POINT('Ctrl Pts',(-1.35438388023453,2.79042020824128,11.1420067497354));
#18737=CARTESIAN_POINT('Ctrl Pts',(-0.294282642636005,3.08774972424349,
11.089386379365));
#18738=CARTESIAN_POINT('Ctrl Pts',(0.65021190135765,2.87407334222539,11.0367660089946));
#18739=CARTESIAN_POINT('Ctrl Pts',(1.59470644535131,2.66039696020728,10.9841456386242));
#18740=CARTESIAN_POINT('Ctrl Pts',(2.42359429574009,1.93571468016887,10.9315252682539));
#18741=CARTESIAN_POINT('Ctrl Pts',(2.76149288344003,1.02821697529914,10.8789048978835));
#18742=CARTESIAN_POINT('Ctrl Pts',(3.09939147113997,0.120719270429434,10.8262845275131));
#18743=CARTESIAN_POINT('Ctrl Pts',(2.9463007961511,-0.969593859271576,10.7736641571428));
#18744=CARTESIAN_POINT('Ctrl Pts',(2.37155179497663,-1.74894687658982,10.7210437867724));
#18745=CARTESIAN_POINT('Ctrl Pts',(1.79680279380215,-2.52829989390807,10.668423416402));
#18746=CARTESIAN_POINT('Ctrl Pts',(0.800395466442055,-2.99669279884355,
10.6158030460317));
#18747=CARTESIAN_POINT('Ctrl Pts',(-0.166422238380945,-2.94200216382593,
10.5631826756613));
#18748=CARTESIAN_POINT('Ctrl Pts',(-1.13323994320395,-2.8873115288083,10.5105623052909));
#18749=CARTESIAN_POINT('Ctrl Pts',(-2.07046802548985,-2.30953735383759,
10.4579419349205));
#18750=CARTESIAN_POINT('Ctrl Pts',(-2.55365933589945,-1.47033910701379,
10.4053215645502));
#18751=CARTESIAN_POINT('Ctrl Pts',(-2.80815619982173,-1.02833338914462,
10.3776064153966));
#18752=CARTESIAN_POINT('Ctrl Pts',(-2.93669740996939,-0.513805263571333,
10.3498912662431));
#18753=CARTESIAN_POINT('Ctrl Pts',(-2.93735377875815,0.0004158914717875,
10.3221761170896));
#18754=CARTESIAN_POINT('Ctrl Pts',(-2.93779053274574,0.00122895754932335,
10.1778238829104));
#18755=CARTESIAN_POINT('Ctrl Pts',(-2.93563218928374,-0.566577199606596,
10.2084385602748));
#18756=CARTESIAN_POINT('Ctrl Pts',(-2.77690932929649,-1.13549932265473,
10.2390532376391));
#18757=CARTESIAN_POINT('Ctrl Pts',(-2.46954008606165,-1.60765366907442,
10.2696679150035));
#18758=CARTESIAN_POINT('Ctrl Pts',(-1.94078749348779,-2.41987818489459,
10.3223328786702));
#18759=CARTESIAN_POINT('Ctrl Pts',(-0.972150510867944,-2.9457409778909,
10.3749978423368));
#18760=CARTESIAN_POINT('Ctrl Pts',(-0.00298230764251388,-2.94672185015728,
10.4276628060035));
#18761=CARTESIAN_POINT('Ctrl Pts',(0.966185895582889,-2.94770272242366,
10.4803277696702));
#18762=CARTESIAN_POINT('Ctrl Pts',(1.93588531941386,-2.42380167396015,10.5329927333369));
#18763=CARTESIAN_POINT('Ctrl Pts',(2.46628089363149,-1.61264909700348,10.5856576970036));
#18764=CARTESIAN_POINT('Ctrl Pts',(2.99667646784912,-0.801496520046785,
10.6383226606703));
#18765=CARTESIAN_POINT('Ctrl Pts',(3.08776819245338,0.296907585403119,10.690987624337));
#18766=CARTESIAN_POINT('Ctrl Pts',(2.69823879520542,1.18435043817229,10.7436525880036));
#18767=CARTESIAN_POINT('Ctrl Pts',(2.30870939795745,2.07179329094149,10.7963175516703));
#18768=CARTESIAN_POINT('Ctrl Pts',(1.43855887885726,2.74827489102996,10.848982515337));
#18769=CARTESIAN_POINT('Ctrl Pts',(0.482469038528927,2.90695754754173,10.9016474790037));
#18770=CARTESIAN_POINT('Ctrl Pts',(-0.473620801799363,3.0656402040535,10.9543124426704));
#18771=CARTESIAN_POINT('Ctrl Pts',(-1.51564996335577,2.70652391698861,11.0069774063371));
#18772=CARTESIAN_POINT('Ctrl Pts',(-2.17097614256679,1.99249620947818,11.0596423700038));
#18773=CARTESIAN_POINT('Ctrl Pts',(-2.66116565955863,1.45839745352016,11.0990362076393));
#18774=CARTESIAN_POINT('Ctrl Pts',(-2.93498842496261,0.725719853723158,
11.1384300452748));
#18775=CARTESIAN_POINT('Ctrl Pts',(-2.94145083142593,-0.00261642954227547,
11.1778238829104));
#18776=CARTESIAN_POINT('Origin',(0.,0.,0.));
#18777=CARTESIAN_POINT('',(-2.9445363666432,0.00211803469319205,12.3221761170896));
#18778=CARTESIAN_POINT('',(-2.94599368555865,0.00130075687149912,12.1778238829104));
#18779=CARTESIAN_POINT('',(-2.942,-3.60291088309151E-16,0.));
#18780=CARTESIAN_POINT('Ctrl Pts',(-2.9445363666432,0.00211803469319205,
12.3221761170896));
#18781=CARTESIAN_POINT('Ctrl Pts',(-2.9456637214079,0.140538485345201,12.3146690440209));
#18782=CARTESIAN_POINT('Ctrl Pts',(-2.93673667551181,0.278812877817704,
12.3071619709522));
#18783=CARTESIAN_POINT('Ctrl Pts',(-2.91725274860024,0.415583368023806,
12.2996548978835));
#18784=CARTESIAN_POINT('Ctrl Pts',(-2.78068135240184,1.37426776932391,12.2470345275131));
#18785=CARTESIAN_POINT('Ctrl Pts',(-2.12542680364205,2.25906209195984,12.1944141571428));
#18786=CARTESIAN_POINT('Ctrl Pts',(-1.24823752065428,2.66926510338839,12.1417937867724));
#18787=CARTESIAN_POINT('Ctrl Pts',(-0.371048237666502,3.07946811481694,
12.089173416402));
#18788=CARTESIAN_POINT('Ctrl Pts',(0.728075779549269,3.01507981503809,12.0365530460316));
#18789=CARTESIAN_POINT('Ctrl Pts',(1.55136877770631,2.50526006508935,11.9839326756613));
#18790=CARTESIAN_POINT('Ctrl Pts',(2.37466177586334,1.99544031514062,11.9313123052909));
#18791=CARTESIAN_POINT('Ctrl Pts',(2.92212375496165,1.04018911502201,11.8786919349205));
#18792=CARTESIAN_POINT('Ctrl Pts',(2.9458228744686,0.0721158274039949,11.8260715645502));
#18793=CARTESIAN_POINT('Ctrl Pts',(2.96952199397554,-0.895957460214037,
11.7734511941798));
#18794=CARTESIAN_POINT('Ctrl Pts',(2.4694582538911,-1.87685283533148,11.7208308238094));
#18795=CARTESIAN_POINT('Ctrl Pts',(1.67209801460167,-2.42634732122405,11.6682104534391));
#18796=CARTESIAN_POINT('Ctrl Pts',(0.874737775312261,-2.9758418071166,11.6155900830687));
#18797=CARTESIAN_POINT('Ctrl Pts',(-0.219918963182118,-3.09393540378431,
11.5629697126983));
#18798=CARTESIAN_POINT('Ctrl Pts',(-1.11612955404462,-2.72714647754463,
11.510349342328));
#18799=CARTESIAN_POINT('Ctrl Pts',(-2.01234014490716,-2.36035755130494,
11.4577289719576));
#18800=CARTESIAN_POINT('Ctrl Pts',(-2.7101045881378,-1.50868610215784,11.4051086015872));
#18801=CARTESIAN_POINT('Ctrl Pts',(-2.89342282416388,-0.557832820042644,
11.3524882312168));
#18802=CARTESIAN_POINT('Ctrl Pts',(-2.9286231547134,-0.375252240171749,
11.3423841931744));
#18803=CARTESIAN_POINT('Ctrl Pts',(-2.94485546023631,-0.189014750280763,
11.332280155132));
#18804=CARTESIAN_POINT('Ctrl Pts',(-2.94318142996902,-0.00248705772575741,
11.3221761170896));
#18805=CARTESIAN_POINT('Ctrl Pts',(-2.94145083142593,-0.00261642954227547,
11.1778238829104));
#18806=CARTESIAN_POINT('Ctrl Pts',(-2.94362790824268,-0.247980760321293,
11.1910950089415));
#18807=CARTESIAN_POINT('Ctrl Pts',(-2.9154621622164,-0.492852393533084,
11.2043661349727));
#18808=CARTESIAN_POINT('Ctrl Pts',(-2.85500395443405,-0.729473081400432,
11.2176372610038));
#18809=CARTESIAN_POINT('Ctrl Pts',(-2.61508239022462,-1.6684755368126,11.2703022246705));
#18810=CARTESIAN_POINT('Ctrl Pts',(-1.86661606494013,-2.4775413196809,11.3229671883372));
#18811=CARTESIAN_POINT('Ctrl Pts',(-0.949093412422085,-2.7896953688222,
11.3756321520039));
#18812=CARTESIAN_POINT('Ctrl Pts',(-0.0315707599040525,-3.10184941796349,
11.4282971156705));
#18813=CARTESIAN_POINT('Ctrl Pts',(1.05500821984753,-2.91709173337779,11.4809620793372));
#18814=CARTESIAN_POINT('Ctrl Pts',(1.81779437152408,-2.31922447800469,11.5336270430039));
#18815=CARTESIAN_POINT('Ctrl Pts',(2.58058052320064,-1.7213572226316,11.5862920066706));
#18816=CARTESIAN_POINT('Ctrl Pts',(3.01957384680218,-0.710380396471107,
11.6389569703373));
#18817=CARTESIAN_POINT('Ctrl Pts',(2.93565629151018,0.255148376847553,11.691621934004));
#18818=CARTESIAN_POINT('Ctrl Pts',(2.85173873621817,1.22067715016623,11.7442868976707));
#18819=CARTESIAN_POINT('Ctrl Pts',(2.24491030203262,2.14075787064307,11.7969518613373));
#18820=CARTESIAN_POINT('Ctrl Pts',(1.39041548234847,2.59806145861508,11.849616825004));
#18821=CARTESIAN_POINT('Ctrl Pts',(0.535920662664327,3.05536504658708,11.9022817886707));
#18822=CARTESIAN_POINT('Ctrl Pts',(-0.566240542518395,3.04989150205426,
11.9549467523374));
#18823=CARTESIAN_POINT('Ctrl Pts',(-1.41615121076395,2.58412350821102,12.0076117160041));
#18824=CARTESIAN_POINT('Ctrl Pts',(-2.26606187900951,2.11835551436778,12.0602766796708));
#18825=CARTESIAN_POINT('Ctrl Pts',(-2.86372201031791,1.19229307121411,12.1129416433374));
#18826=CARTESIAN_POINT('Ctrl Pts',(-2.93804565964555,0.22597844177242,12.1656066070041));
#18827=CARTESIAN_POINT('Ctrl Pts',(-2.94379288681505,0.151256200025011,
12.1696790323062));
#18828=CARTESIAN_POINT('Ctrl Pts',(-2.94641083929854,0.0762932715455572,
12.1737514576083));
#18829=CARTESIAN_POINT('Ctrl Pts',(-2.94599368555865,0.00130075687149912,
12.1778238829104));
#18830=CARTESIAN_POINT('Origin',(0.,0.,0.));
#18831=CARTESIAN_POINT('',(-2.93733773658367,0.000353650820144602,13.3221761170896));
#18832=CARTESIAN_POINT('',(-2.93794966127546,0.0013934910171998,13.1778238829104));
#18833=CARTESIAN_POINT('',(-2.942,-3.60291088309151E-16,0.));
#18834=CARTESIAN_POINT('Ctrl Pts',(-2.93733773658367,0.000353650820144602,
13.3221761170896));
#18835=CARTESIAN_POINT('Ctrl Pts',(-2.93784318272048,0.466397170874405,
13.2970579329098));
#18836=CARTESIAN_POINT('Ctrl Pts',(-2.8333193685149,0.932226520914598,13.27193974873));
#18837=CARTESIAN_POINT('Ctrl Pts',(-2.62254748003497,1.34362161549686,13.2468215645502));
#18838=CARTESIAN_POINT('Ctrl Pts',(-2.18099904818651,2.20545788879211,13.1942011941798));
#18839=CARTESIAN_POINT('Ctrl Pts',(-1.27316460447925,2.82840106158337,13.1415808238094));
#18840=CARTESIAN_POINT('Ctrl Pts',(-0.31018098965669,2.93033473129373,13.0889604534391));
#18841=CARTESIAN_POINT('Ctrl Pts',(0.652802625165875,3.03226840100409,13.0363400830687));
#18842=CARTESIAN_POINT('Ctrl Pts',(1.67093541110377,2.61319256763355,12.9837197126983));
#18843=CARTESIAN_POINT('Ctrl Pts',(2.28313120153524,1.86289672775273,12.9310993423279));
#18844=CARTESIAN_POINT('Ctrl Pts',(2.89532699196672,1.1126008878719,12.8784789719576));
#18845=CARTESIAN_POINT('Ctrl Pts',(3.10158578689178,0.0310850414808014,
12.8258586015872));
#18846=CARTESIAN_POINT('Ctrl Pts',(2.80849777284497,-0.891859624755379,
12.7732382312168));
#18847=CARTESIAN_POINT('Ctrl Pts',(2.51540975879817,-1.81480429099155,12.7206178608465));
#18848=CARTESIAN_POINT('Ctrl Pts',(1.72297493577951,-2.57917777707278,12.6679974904761));
#18849=CARTESIAN_POINT('Ctrl Pts',(0.790067400131255,-2.83881430845519,
12.6153771201057));
#18850=CARTESIAN_POINT('Ctrl Pts',(-0.142840135516982,-3.0984508398376,
12.5627567497353));
#18851=CARTESIAN_POINT('Ctrl Pts',(-1.21622038379481,-2.85335041652122,
12.510136379365));
#18852=CARTESIAN_POINT('Ctrl Pts',(-1.94396638611522,-2.21451296488091,
12.4575160089946));
#18853=CARTESIAN_POINT('Ctrl Pts',(-2.56788867194677,-1.66681511174075,
12.4124027116929));
#18854=CARTESIAN_POINT('Ctrl Pts',(-2.93776159700942,-0.829711212970877,
12.3672894143913));
#18855=CARTESIAN_POINT('Ctrl Pts',(-2.9445363666432,0.00211803469319205,
12.3221761170896));
#18856=CARTESIAN_POINT('Ctrl Pts',(-2.94599368555865,0.00130075687149912,
12.1778238829104));
#18857=CARTESIAN_POINT('Ctrl Pts',(-2.94101617029297,-0.893516551252978,
12.226416421275));
#18858=CARTESIAN_POINT('Ctrl Pts',(-2.50391622116005,-1.79254618589271,
12.2750089596396));
#18859=CARTESIAN_POINT('Ctrl Pts',(-1.79466984706922,-2.33716467042755,
12.3236014980042));
#18860=CARTESIAN_POINT('Ctrl Pts',(-1.02598321781837,-2.92742633745608,
12.3762664616709));
#18861=CARTESIAN_POINT('Ctrl Pts',(0.0623772080302214,-3.10138285578342,
12.4289314253375));
#18862=CARTESIAN_POINT('Ctrl Pts',(0.976754244976282,-2.78013123936204,
12.4815963890042));
#18863=CARTESIAN_POINT('Ctrl Pts',(1.89113128192235,-2.45887962294065,12.5342613526709));
#18864=CARTESIAN_POINT('Ctrl Pts',(2.6315249299659,-1.64241987177053,12.5869263163376));
#18865=CARTESIAN_POINT('Ctrl Pts',(2.86210835815027,-0.701080799331296,
12.6395912800043));
#18866=CARTESIAN_POINT('Ctrl Pts',(3.09269178633465,0.240258273107937,12.692256243671));
#18867=CARTESIAN_POINT('Ctrl Pts',(2.81346499465986,1.30647666681628,12.7449212073377));
#18868=CARTESIAN_POINT('Ctrl Pts',(2.15107931219979,2.01396036610533,12.7975861710043));
#18869=CARTESIAN_POINT('Ctrl Pts',(1.48869362973973,2.72144406539436,12.850251134671));
#18870=CARTESIAN_POINT('Ctrl Pts',(0.443149056494409,3.07019307026412,12.9029160983377));
#18871=CARTESIAN_POINT('Ctrl Pts',(-0.511317558922748,2.90202221756343,
12.9555810620044));
#18872=CARTESIAN_POINT('Ctrl Pts',(-1.46578417433991,2.73385136486274,13.0082460256711));
#18873=CARTESIAN_POINT('Ctrl Pts',(-2.3291728319289,2.04876065459161,13.0609109893378));
#18874=CARTESIAN_POINT('Ctrl Pts',(-2.7098688231833,1.1574927237348,13.1135759530044));
#18875=CARTESIAN_POINT('Ctrl Pts',(-2.86467717936984,0.795062526234979,
13.1349919296398));
#18876=CARTESIAN_POINT('Ctrl Pts',(-2.93966715879244,0.398538727939818,
13.1564079062751));
#18877=CARTESIAN_POINT('Ctrl Pts',(-2.93794966127546,0.0013934910171998,
13.1778238829104));
#18878=CARTESIAN_POINT('Origin',(0.,0.,0.));
#18879=CARTESIAN_POINT('',(-2.94325266537063,-0.0024318079996577,14.3221761170896));
#18880=CARTESIAN_POINT('',(-2.94111188951679,-0.00259486169482749,14.1778238829104));
#18881=CARTESIAN_POINT('',(-2.942,-3.60291088309151E-16,0.));
#18882=CARTESIAN_POINT('Ctrl Pts',(-2.94325266537063,-0.0024318079996577,
14.3221761170896));
#18883=CARTESIAN_POINT('Ctrl Pts',(-2.93620194204164,0.786300619982285,
14.2794468217987));
#18884=CARTESIAN_POINT('Ctrl Pts',(-2.60854122084458,1.58016790859219,14.2367175265078));
#18885=CARTESIAN_POINT('Ctrl Pts',(-2.04150376744995,2.12493551247607,14.1939882312168));
#18886=CARTESIAN_POINT('Ctrl Pts',(-1.34320718641939,2.79580716825642,14.1413678608465));
#18887=CARTESIAN_POINT('Ctrl Pts',(-0.281884150596186,3.08890703892681,
14.0887474904761));
#18888=CARTESIAN_POINT('Ctrl Pts',(0.661753798897932,2.87144767774516,14.0361271201057));
#18889=CARTESIAN_POINT('Ctrl Pts',(1.60539174839208,2.65398831656351,13.9835067497354));
#18890=CARTESIAN_POINT('Ctrl Pts',(2.43134461155714,1.92596972352975,13.930886379365));
#18891=CARTESIAN_POINT('Ctrl Pts',(2.76559296922098,1.01711939779235,13.8782660089946));
#18892=CARTESIAN_POINT('Ctrl Pts',(3.09984132688481,0.108269072054953,13.8256456386242));
#18893=CARTESIAN_POINT('Ctrl Pts',(2.94238517904746,-0.981412986386104,
13.7730252682539));
#18894=CARTESIAN_POINT('Ctrl Pts',(2.36451469520878,-1.75845069530582,13.7204048978835));
#18895=CARTESIAN_POINT('Ctrl Pts',(1.7866442113701,-2.53548840422553,13.6677845275131));
#18896=CARTESIAN_POINT('Ctrl Pts',(0.788359391530092,-2.99988176362388,
13.6151641571428));
#18897=CARTESIAN_POINT('Ctrl Pts',(-0.178232238982059,-2.94131149038551,
13.5625437867724));
#18898=CARTESIAN_POINT('Ctrl Pts',(-1.14482386949421,-2.88274121714715,
13.509923416402));
#18899=CARTESIAN_POINT('Ctrl Pts',(-2.07972231067849,-2.30120731127206,
13.4573030460317));
#18900=CARTESIAN_POINT('Ctrl Pts',(-2.5595403212758,-1.46007567143488,13.4046826756613));
#18901=CARTESIAN_POINT('Ctrl Pts',(-2.81031856879004,-1.02045582826861,
13.3771804894707));
#18902=CARTESIAN_POINT('Ctrl Pts',(-2.9367843178467,-0.509922711901109,
13.3496783032802));
#18903=CARTESIAN_POINT('Ctrl Pts',(-2.93733773658367,0.000353650820144602,
13.3221761170896));
#18904=CARTESIAN_POINT('Ctrl Pts',(-2.93794966127546,0.0013934910171998,
13.1778238829104));
#18905=CARTESIAN_POINT('Ctrl Pts',(-2.9354435856223,-0.578098472832708,
13.2090728699418));
#18906=CARTESIAN_POINT('Ctrl Pts',(-2.76961959866241,-1.15891354184382,
13.2403218569731));
#18907=CARTESIAN_POINT('Ctrl Pts',(-2.45014221851649,-1.63706498032062,
13.2715708440045));
#18908=CARTESIAN_POINT('Ctrl Pts',(-1.91171629767549,-2.44290960207673,
13.3242358076712));
#18909=CARTESIAN_POINT('Ctrl Pts',(-0.936861131073665,-2.95715369414646,
13.3769007713379));
#18910=CARTESIAN_POINT('Ctrl Pts',(0.032249473718084,-2.94654692146698,
13.4295657350046));
#18911=CARTESIAN_POINT('Ctrl Pts',(1.00136007850986,-2.9359401487875,13.4822306986712));
#18912=CARTESIAN_POINT('Ctrl Pts',(1.96472612149158,-2.40048251135878,13.5348956623379));
#18913=CARTESIAN_POINT('Ctrl Pts',(2.48538560527679,-1.58304647931889,13.5875606260046));
#18914=CARTESIAN_POINT('Ctrl Pts',(3.00604508906198,-0.765610447279041,
13.6402255896713));
#18915=CARTESIAN_POINT('Ctrl Pts',(3.08399801365073,0.333803979371919,13.692890553338));
#18916=CARTESIAN_POINT('Ctrl Pts',(2.68388585052197,1.21652624548705,13.7455555170047));
#18917=CARTESIAN_POINT('Ctrl Pts',(2.28377368739319,2.0992485116022,13.7982204806713));
#18918=CARTESIAN_POINT('Ctrl Pts',(1.40559643654686,2.76527861718149,13.850885444338));
#18919=CARTESIAN_POINT('Ctrl Pts',(0.447678061833244,2.91251851826326,13.9035504080047));
#18920=CARTESIAN_POINT('Ctrl Pts',(-0.510240312880357,3.05975841934504,
13.9562153716714));
#18921=CARTESIAN_POINT('Ctrl Pts',(-1.54789981146125,2.68820811592931,14.0088803353381));
#18922=CARTESIAN_POINT('Ctrl Pts',(-2.1946428070508,1.96639671204873,14.0615452990048));
#18923=CARTESIAN_POINT('Ctrl Pts',(-2.67062249982462,1.435169358057,14.1003048269733));
#18924=CARTESIAN_POINT('Ctrl Pts',(-2.93486488519192,0.714225423327012,
14.1390643549419));
#18925=CARTESIAN_POINT('Ctrl Pts',(-2.94111188951679,-0.00259486169482749,
14.1778238829104));
#18926=CARTESIAN_POINT('Origin',(0.,0.,-1.84858989190501));
#18927=CARTESIAN_POINT('',(-2.37275986033066,-0.00196044888638088,14.651410108095));
#18928=CARTESIAN_POINT('',(-2.37517539399571,0.0009292342096269,14.848589891905));
#18929=CARTESIAN_POINT('',(-2.37175,-2.62313128856983E-13,-1.84858989190501));
#18930=CARTESIAN_POINT('',(-2.34668236863853,0.343918483395512,15.62825));
#18931=CARTESIAN_POINT('Ctrl Pts',(-2.37275986033066,-0.00196044888638126,
14.651410108095));
#18932=CARTESIAN_POINT('Ctrl Pts',(-2.37407562336888,-0.149148890039704,
14.6613011831744));
#18933=CARTESIAN_POINT('Ctrl Pts',(-2.29486163858049,-1.07797575416432,
14.7238126286243));
#18934=CARTESIAN_POINT('Ctrl Pts',(-1.07036982067409,-2.58532778276268,
14.8389444444444));
#18935=CARTESIAN_POINT('Ctrl Pts',(1.57881200919325,-2.30987053095853,14.9968055555556));
#18936=CARTESIAN_POINT('Ctrl Pts',(2.79654399706859,0.0566462213665858,
15.1546666666667));
#18937=CARTESIAN_POINT('Ctrl Pts',(1.48409012818578,2.37398300468726,15.3125277777778));
#18938=CARTESIAN_POINT('Ctrl Pts',(-1.17817012667699,2.53688639776398,15.4703888888889));
#18939=CARTESIAN_POINT('Ctrl Pts',(-2.23297482288527,1.11978691060522,15.5756296296296));
#18940=CARTESIAN_POINT('Ctrl Pts',(-2.34668236863854,0.343918483395395,
15.62825));
#18941=CARTESIAN_POINT('',(-0.439445221994505,2.33068358199182,15.62825));
#18942=CARTESIAN_POINT('Origin',(0.,0.,15.62825));
#18943=CARTESIAN_POINT('Ctrl Pts',(-2.37517539399571,0.000929234209626874,
14.848589891905));
#18944=CARTESIAN_POINT('Ctrl Pts',(-2.37154287511732,-0.72977569986937,
14.8978167399366));
#18945=CARTESIAN_POINT('Ctrl Pts',(-1.620069408967,-2.24871933567263,14.9997085516349));
#18946=CARTESIAN_POINT('Ctrl Pts',(0.958368222991996,-2.62865236842956,
15.1542653269999));
#18947=CARTESIAN_POINT('Ctrl Pts',(2.7277014223945,-0.634378452891388,15.3122602179999));
#18948=CARTESIAN_POINT('Ctrl Pts',(2.01676643438217,1.93930517753648,15.470255109));
#18949=CARTESIAN_POINT('Ctrl Pts',(0.331786659212352,2.47609764328476,15.5755850363333));
#18950=CARTESIAN_POINT('Ctrl Pts',(-0.439445221994538,2.33068358199181,
15.62825));
#18951=CARTESIAN_POINT('Origin',(0.,0.,-1.84858989190501));
#18952=CARTESIAN_POINT('',(-2.36799142649297,0.000285102424211894,13.651410108095));
#18953=CARTESIAN_POINT('',(-2.37103403261776,-0.00209189776527924,13.848589891905));
#18954=CARTESIAN_POINT('',(-2.37175,-2.62313128856983E-13,-1.84858989190501));
#18955=CARTESIAN_POINT('Ctrl Pts',(-2.36799142649297,0.000285102424211897,
13.651410108095));
#18956=CARTESIAN_POINT('Ctrl Pts',(-2.36754527731231,-0.41108402173757,
13.6789122942855));
#18957=CARTESIAN_POINT('Ctrl Pts',(-2.07052456040773,-1.61013525385437,
13.7590348508465));
#18958=CARTESIAN_POINT('Ctrl Pts',(-0.16923542984156,-2.79279215602584,
13.8917777777778));
#18959=CARTESIAN_POINT('Ctrl Pts',(2.24512421134353,-1.66965318578134,14.0496388888889));
#18960=CARTESIAN_POINT('Ctrl Pts',(2.62593313585052,0.965751391486786,14.2075));
#18961=CARTESIAN_POINT('Ctrl Pts',(0.628359679142483,2.72647005025058,14.3653611111111));
#18962=CARTESIAN_POINT('Ctrl Pts',(-1.77762972544941,2.06202090562868,14.5133311471428));
#18963=CARTESIAN_POINT('Ctrl Pts',(-2.36707578383325,0.633891398858792,
14.6086808128041));
#18964=CARTESIAN_POINT('Ctrl Pts',(-2.37275986033066,-0.00196044888638126,
14.651410108095));
#18965=CARTESIAN_POINT('Ctrl Pts',(-2.37103403261776,-0.00209189776527889,
13.848589891905));
#18966=CARTESIAN_POINT('Ctrl Pts',(-2.37284080801943,-0.20941258958213,
13.8624953276032));
#18967=CARTESIAN_POINT('Ctrl Pts',(-2.25333213139831,-1.19988405133594,
13.929065726968));
#18968=CARTESIAN_POINT('Ctrl Pts',(-0.869666078203209,-2.66015561356989,
14.0483010899995));
#18969=CARTESIAN_POINT('Ctrl Pts',(1.75267763866885,-2.18191305067097,14.2062959809995));
#18970=CARTESIAN_POINT('Ctrl Pts',(2.78512620401791,0.275629071355557,14.3642908719996));
#18971=CARTESIAN_POINT('Ctrl Pts',(1.29091271455523,2.48320730756548,14.5222857629997));
#18972=CARTESIAN_POINT('Ctrl Pts',(-1.37414448785656,2.43798182357128,14.6802806539997));
#18973=CARTESIAN_POINT('Ctrl Pts',(-2.35095938458833,0.884486526760038,
14.7890486969682));
#18974=CARTESIAN_POINT('Ctrl Pts',(-2.37542909742077,0.0519633377314283,
14.8451517762699));
#18975=CARTESIAN_POINT('Ctrl Pts',(-2.37517539399571,0.000929234209626874,
14.848589891905));
#18976=CARTESIAN_POINT('Origin',(0.,0.,-1.84858989190501));
#18977=CARTESIAN_POINT('',(-2.3737947408518,0.00170749448784205,12.651410108095));
#18978=CARTESIAN_POINT('',(-2.36848474137664,0.00112338963946246,12.848589891905));
#18979=CARTESIAN_POINT('',(-2.37175,-2.62313128856983E-13,-1.84858989190501));
#18980=CARTESIAN_POINT('Ctrl Pts',(-2.3737947408518,0.00170749448784207,
12.651410108095));
#18981=CARTESIAN_POINT('Ctrl Pts',(-2.36833312974404,-0.668887685031927,
12.6965234053967));
#18982=CARTESIAN_POINT('Ctrl Pts',(-1.72235411599047,-2.13088047848934,
12.7942570730687));
#18983=CARTESIAN_POINT('Ctrl Pts',(0.750172845833004,-2.69546828972993,
12.9446111111111));
#18984=CARTESIAN_POINT('Ctrl Pts',(2.66668266040929,-0.846825037914988,
13.1024722222222));
#18985=CARTESIAN_POINT('Ctrl Pts',(2.16784415239069,1.76882949166842,13.2603333333333));
#18986=CARTESIAN_POINT('Ctrl Pts',(-0.294517949969841,2.78236767093066,
13.4181944444444));
#18987=CARTESIAN_POINT('Ctrl Pts',(-2.10760963637491,1.5382497642797,13.548553369365));
#18988=CARTESIAN_POINT('Ctrl Pts',(-2.36839890163746,0.375995067988055,
13.6262919239152));
#18989=CARTESIAN_POINT('Ctrl Pts',(-2.36799142649297,0.000285102424211897,
13.651410108095));
#18990=CARTESIAN_POINT('Ctrl Pts',(-2.36848474137664,0.00112338963946246,
12.848589891905));
#18991=CARTESIAN_POINT('Ctrl Pts',(-2.36646442019019,-0.466045225337024,
12.8798388789364));
#18992=CARTESIAN_POINT('Ctrl Pts',(-2.00748312661735,-1.72341304420753,
12.9637528296344));
#18993=CARTESIAN_POINT('Ctrl Pts',(0.0306296239850783,-2.7985342282319,
13.1003317439992));
#18994=CARTESIAN_POINT('Ctrl Pts',(2.36053793034993,-1.50352574600393,13.2583266349992));
#18995=CARTESIAN_POINT('Ctrl Pts',(2.54906768788899,1.15541663986578,13.4163215259993));
#18996=CARTESIAN_POINT('Ctrl Pts',(0.42518914129335,2.76621565710669,13.5743164169993));
#18997=CARTESIAN_POINT('Ctrl Pts',(-1.86352481270074,1.94670562977947,13.7184058723013));
#18998=CARTESIAN_POINT('Ctrl Pts',(-2.36599788968529,0.57578658999839,13.8098303639365));
#18999=CARTESIAN_POINT('Ctrl Pts',(-2.37103403261776,-0.00209189776527889,
13.848589891905));
#19000=CARTESIAN_POINT('Origin',(0.,0.,-1.84858989190501));
#19001=CARTESIAN_POINT('',(-2.37270243253876,-0.00200498951788303,11.651410108095));
#19002=CARTESIAN_POINT('',(-2.37496958658182,0.00104863022067879,11.848589891905));
#19003=CARTESIAN_POINT('',(-2.37175,-2.62313128856983E-13,-1.84858989190501));
#19004=CARTESIAN_POINT('Ctrl Pts',(-2.37270243253876,-0.00200498951788284,
11.651410108095));
#19005=CARTESIAN_POINT('Ctrl Pts',(-2.37405198430164,-0.152377883745359,
11.6615141461374));
#19006=CARTESIAN_POINT('Ctrl Pts',(-2.29281607417404,-1.08441874324097,
11.7242385545502));
#19007=CARTESIAN_POINT('Ctrl Pts',(-1.05977053720295,-2.58943908287633,
11.8395833333333));
#19008=CARTESIAN_POINT('Ctrl Pts',(1.58766534266525,-2.30382879610199,11.9974444444444));
#19009=CARTESIAN_POINT('Ctrl Pts',(2.79707340746319,0.0684743370742143,
12.1553055555555));
#19010=CARTESIAN_POINT('Ctrl Pts',(1.47303233105958,2.37875683253439,12.3131666666667));
#19011=CARTESIAN_POINT('Ctrl Pts',(-1.18520769732058,2.53448043892505,12.4710277777778));
#19012=CARTESIAN_POINT('Ctrl Pts',(-2.31706196946124,1.00613052370996,12.5837755915872));
#19013=CARTESIAN_POINT('Ctrl Pts',(-2.37470357962243,0.113297808503467,
12.6439030350263));
#19014=CARTESIAN_POINT('Ctrl Pts',(-2.3737947408518,0.00170749448784207,
12.651410108095));
#19015=CARTESIAN_POINT('Ctrl Pts',(-2.37496958658182,0.00104863022067909,
11.848589891905));
#19016=CARTESIAN_POINT('Ctrl Pts',(-2.37095686672064,-0.72032558818314,
11.8971824302696));
#19017=CARTESIAN_POINT('Ctrl Pts',(-1.63667192852724,-2.23060698037937,
11.9984399323009));
#19018=CARTESIAN_POINT('Ctrl Pts',(0.927689321261817,-2.64047796075702,
12.1523623979988));
#19019=CARTESIAN_POINT('Ctrl Pts',(2.71833714731268,-0.66586366962402,12.3103572889989));
#19020=CARTESIAN_POINT('Ctrl Pts',(2.04302496870488,1.91279385105346,12.468352179999));
#19021=CARTESIAN_POINT('Ctrl Pts',(-0.48563275555883,2.75624604578475,12.626347070999));
#19022=CARTESIAN_POINT('Ctrl Pts',(-2.16074812800628,1.4270578867686,12.7530929749677));
#19023=CARTESIAN_POINT('Ctrl Pts',(-2.36986933510064,0.32128967640745,12.8271739152697));
#19024=CARTESIAN_POINT('Ctrl Pts',(-2.36848474137664,0.00112338963946246,
12.848589891905));
#19025=CARTESIAN_POINT('Origin',(0.,0.,-1.84858989190501));
#19026=CARTESIAN_POINT('',(-2.3680043592011,0.000335278925106314,10.651410108095));
#19027=CARTESIAN_POINT('',(-2.37130727717011,-0.00210928510120167,10.848589891905));
#19028=CARTESIAN_POINT('',(-2.37175,-2.62313128856983E-13,-1.84858989190501));
#19029=CARTESIAN_POINT('Ctrl Pts',(-2.3680043592011,0.000335278925106194,
10.651410108095));
#19030=CARTESIAN_POINT('Ctrl Pts',(-2.36747521485208,-0.414214015593381,
10.6791252572485));
#19031=CARTESIAN_POINT('Ctrl Pts',(-2.06710351553143,-1.61654972761244,
10.7594607767724));
#19032=CARTESIAN_POINT('Ctrl Pts',(-0.158018739337926,-2.79344562132492,
10.8924166666667));
#19033=CARTESIAN_POINT('Ctrl Pts',(2.25180017160661,-1.66063371893121,11.0502777777778));
#19034=CARTESIAN_POINT('Ctrl Pts',(2.62205116590109,0.976297109112734,11.2081388888889));
#19035=CARTESIAN_POINT('Ctrl Pts',(0.617379419647229,2.72894686881467,11.366));
#19036=CARTESIAN_POINT('Ctrl Pts',(-1.78238141625357,2.05587933285381,11.5137570730687));
#19037=CARTESIAN_POINT('Ctrl Pts',(-2.36702371369352,0.630742424660346,
11.608893775767));
#19038=CARTESIAN_POINT('Ctrl Pts',(-2.37270243253876,-0.00200498951788284,
11.651410108095));
#19039=CARTESIAN_POINT('Ctrl Pts',(-2.37130727717011,-0.00210928510120129,
10.848589891905));
#19040=CARTESIAN_POINT('Ctrl Pts',(-2.37306236960384,-0.199914469168129,
10.8618610179362));
#19041=CARTESIAN_POINT('Ctrl Pts',(-2.26024839139859,-1.18071373741556,
10.927797107634));
#19042=CARTESIAN_POINT('Ctrl Pts',(-0.90141796228012,-2.64956165719617,
11.0463981609985));
#19043=CARTESIAN_POINT('Ctrl Pts',(1.72648179491819,-2.20272375262492,11.2043930519985));
#19044=CARTESIAN_POINT('Ctrl Pts',(2.7881905800153,0.242331605070017,11.3623879429986));
#19045=CARTESIAN_POINT('Ctrl Pts',(1.32057126786748,2.46755402056041,11.5203828339987));
#19046=CARTESIAN_POINT('Ctrl Pts',(-1.34501422335496,2.45431621031658,11.6783777249987));
#19047=CARTESIAN_POINT('Ctrl Pts',(-2.34590203170026,0.903460530701682,
11.7877800776342));
#19048=CARTESIAN_POINT('Ctrl Pts',(-2.37530588310888,0.0615052912262518,
11.8445174666029));
#19049=CARTESIAN_POINT('Ctrl Pts',(-2.37496958658182,0.00104863022067909,
11.848589891905));
#19050=CARTESIAN_POINT('Origin',(0.,0.,-1.84858989190501));
#19051=CARTESIAN_POINT('',(-2.37387835550442,0.0016747535505271,9.65141010809499));
#19052=CARTESIAN_POINT('',(-2.36835645684558,0.000990747813277848,9.84858989190503));
#19053=CARTESIAN_POINT('',(-2.37175,-2.62313128856983E-13,-1.84858989190501));
#19054=CARTESIAN_POINT('Ctrl Pts',(-2.37387835550442,0.00167475355052717,
9.65141010809499));
#19055=CARTESIAN_POINT('Ctrl Pts',(-2.36846517734921,-0.672024104003181,
9.69673636835963));
#19056=CARTESIAN_POINT('Ctrl Pts',(-1.71729169385484,-2.1369916722257,9.79468299899462));
#19057=CARTESIAN_POINT('Ctrl Pts',(0.760987165659879,-2.69243512365168,
9.94525));
#19058=CARTESIAN_POINT('Ctrl Pts',(2.6700603672968,-0.836113626465368,10.1031111111111));
#19059=CARTESIAN_POINT('Ctrl Pts',(2.16072649637127,1.7775177549783,10.2609722222222));
#19060=CARTESIAN_POINT('Ctrl Pts',(-0.305685313585232,2.78116249982291,
10.4188333333333));
#19061=CARTESIAN_POINT('Ctrl Pts',(-2.11081288774265,1.53182193243431,10.5489792952909));
#19062=CARTESIAN_POINT('Ctrl Pts',(-2.36847985572451,0.37285508129321,10.6265048868781));
#19063=CARTESIAN_POINT('Ctrl Pts',(-2.3680043592011,0.000335278925106194,
10.651410108095));
#19064=CARTESIAN_POINT('Ctrl Pts',(-2.36835645684558,0.00099074781327764,
9.84858989190503));
#19065=CARTESIAN_POINT('Ctrl Pts',(-2.36661646666674,-0.456757128880904,
9.87920456926939));
#19066=CARTESIAN_POINT('Ctrl Pts',(-2.01853982608692,-1.70439405627733,
9.96248421030043));
#19067=CARTESIAN_POINT('Ctrl Pts',(-0.00283249851198579,-2.79870028674429,
10.0984288149982));
#19068=CARTESIAN_POINT('Ctrl Pts',(2.34239313895008,-1.53164150527581,10.2564237059982));
#19069=CARTESIAN_POINT('Ctrl Pts',(2.56269918704329,1.12485741087042,10.4144185969983));
#19070=CARTESIAN_POINT('Ctrl Pts',(0.458233353927178,2.76093344928963,10.5724134879983));
#19071=CARTESIAN_POINT('Ctrl Pts',(-1.85023633825226,1.96536160231837,10.7171372529672));
#19072=CARTESIAN_POINT('Ctrl Pts',(-2.36609748365237,0.585053046589831,
10.8091960542695));
#19073=CARTESIAN_POINT('Ctrl Pts',(-2.37130727717011,-0.00210928510120129,
10.848589891905));
#19074=CARTESIAN_POINT('Origin',(0.,0.,-1.84858989190501));
#19075=CARTESIAN_POINT('',(-2.37260887298938,-0.00202072084187682,8.65141010809499));
#19076=CARTESIAN_POINT('',(-2.3747901511292,0.00119133359606532,8.84858989190503));
#19077=CARTESIAN_POINT('',(-2.37175,-2.62313128856983E-13,-1.84858989190501));
#19078=CARTESIAN_POINT('Ctrl Pts',(-2.37260887298937,-0.00202072084187674,
8.65141010809499));
#19079=CARTESIAN_POINT('Ctrl Pts',(-2.37399141457934,-0.155578652695773,
8.66172710910036));
#19080=CARTESIAN_POINT('Ctrl Pts',(-2.29073220490892,-1.09084435213441,
8.72466448047611));
#19081=CARTESIAN_POINT('Ctrl Pts',(-1.04936735270146,-2.59367240037321,
8.84022222222223));
#19082=CARTESIAN_POINT('Ctrl Pts',(1.59690068918271,-2.29743695240177,8.99808333333332));
#19083=CARTESIAN_POINT('Ctrl Pts',(2.79677599470576,0.0797019247629725,
9.15594444444445));
#19084=CARTESIAN_POINT('Ctrl Pts',(1.46347155312646,2.38465078671139,9.31380555555555));
#19085=CARTESIAN_POINT('Ctrl Pts',(-1.19537219008389,2.52970229247383,9.47166666666666));
#19086=CARTESIAN_POINT('Ctrl Pts',(-2.31895585283185,0.999716542450464,
9.58420151751315));
#19087=CARTESIAN_POINT('Ctrl Pts',(-2.37474946901026,0.110089469797055,
9.64411599798926));
#19088=CARTESIAN_POINT('Ctrl Pts',(-2.37387835550442,0.00167475355052717,
9.65141010809499));
#19089=CARTESIAN_POINT('Ctrl Pts',(-2.3747901511292,0.00119133359606537,
8.84858989190503));
#19090=CARTESIAN_POINT('Ctrl Pts',(-2.37038906205444,-0.71090872088079,
8.89654812060261));
#19091=CARTESIAN_POINT('Ctrl Pts',(-1.65267775677864,-2.21269450774448,
8.99717131296688));
#19092=CARTESIAN_POINT('Ctrl Pts',(0.896053003445084,-2.6513808351669,9.15045946899784));
#19093=CARTESIAN_POINT('Ctrl Pts',(2.71018167460651,-0.698316982967359,
9.30845435999788));
#19094=CARTESIAN_POINT('Ctrl Pts',(2.06574861445826,1.88823038317285,9.46644925099794));
#19095=CARTESIAN_POINT('Ctrl Pts',(-0.45264386973844,2.76185532663481,9.62444414199799));
#19096=CARTESIAN_POINT('Ctrl Pts',(-2.15199374797492,1.44623886325989,9.75182435563369));
#19097=CARTESIAN_POINT('Ctrl Pts',(-2.36960968846224,0.330684626839437,
9.8265396056027));
#19098=CARTESIAN_POINT('Ctrl Pts',(-2.36835645684558,0.00099074781327764,
9.84858989190503));
#19099=CARTESIAN_POINT('Origin',(0.,0.,-1.84858989190501));
#19100=CARTESIAN_POINT('',(-2.36801892187683,0.000385579322849399,7.65141010809499));
#19101=CARTESIAN_POINT('',(-2.37158591103805,-0.00211396583053219,7.84858989190503));
#19102=CARTESIAN_POINT('',(-2.37175,-2.62313128856983E-13,-1.84858989190501));
#19103=CARTESIAN_POINT('Ctrl Pts',(-2.36801892187683,0.000385579322849869,
7.65141010809499));
#19104=CARTESIAN_POINT('Ctrl Pts',(-2.36740549965901,-0.417342685994756,
7.67933822021147));
#19105=CARTESIAN_POINT('Ctrl Pts',(-2.06366306314178,-1.62296175556451,
7.75988670269832));
#19106=CARTESIAN_POINT('Ctrl Pts',(-0.146803886877873,-2.79405744038503,
7.89305555555557));
#19107=CARTESIAN_POINT('Ctrl Pts',(2.25844822171206,-1.65158105802259,8.05091666666665));
#19108=CARTESIAN_POINT('Ctrl Pts',(2.61811094239596,0.986814802625037,8.20877777777778));
#19109=CARTESIAN_POINT('Ctrl Pts',(0.606419780073446,2.73140319464357,8.36663888888888));
#19110=CARTESIAN_POINT('Ctrl Pts',(-1.7871649975578,2.04969182184781,8.51418299899463));
#19111=CARTESIAN_POINT('Ctrl Pts',(-2.36693996130543,0.627621353124904,
8.60910673873));
#19112=CARTESIAN_POINT('Ctrl Pts',(-2.37260887298937,-0.00202072084187674,
8.65141010809499));
#19113=CARTESIAN_POINT('Ctrl Pts',(-2.37158591103805,-0.002113965830532,
7.84858989190503));
#19114=CARTESIAN_POINT('Ctrl Pts',(-2.37327853101496,-0.190408271679788,
7.86122670826915));
#19115=CARTESIAN_POINT('Ctrl Pts',(-2.26703071089283,-1.16154754141212,
7.92652848829996));
#19116=CARTESIAN_POINT('Ctrl Pts',(-0.9330321424437,-2.63859476601473,8.04449523199746));
#19117=CARTESIAN_POINT('Ctrl Pts',(1.70002224901497,-2.22320841823872,8.2024901229975));
#19118=CARTESIAN_POINT('Ctrl Pts',(2.79088864512093,0.208978201275766,8.36048501399757));
#19119=CARTESIAN_POINT('Ctrl Pts',(1.34997937336987,2.45158867054595,8.51847990499762));
#19120=CARTESIAN_POINT('Ctrl Pts',(-1.31557386100644,2.47022200101732,8.67647479599767));
#19121=CARTESIAN_POINT('Ctrl Pts',(-2.34084261733164,0.922522196646213,
8.78651145830014));
#19122=CARTESIAN_POINT('Ctrl Pts',(-2.37522208450983,0.0710785316625285,
8.84388315693593));
#19123=CARTESIAN_POINT('Ctrl Pts',(-2.3747901511292,0.00119133359606537,
8.84858989190503));
#19124=CARTESIAN_POINT('Origin',(0.,0.,-1.84858989190501));
#19125=CARTESIAN_POINT('',(-2.37396076251026,0.0016408096299993,6.65141010809499));
#19126=CARTESIAN_POINT('',(-2.36824488832617,0.00085307042009708,6.84858989190503));
#19127=CARTESIAN_POINT('',(-2.37175,-2.62313128856983E-13,-1.84858989190501));
#19128=CARTESIAN_POINT('Ctrl Pts',(-2.37396076251026,0.00164080962999946,
6.65141010809499));
#19129=CARTESIAN_POINT('Ctrl Pts',(-2.36860111288507,-0.675161988858878,
6.69694933132258));
#19130=CARTESIAN_POINT('Ctrl Pts',(-1.71220786555833,-2.14309654094568,
6.79510892492056));
#19131=CARTESIAN_POINT('Ctrl Pts',(0.771789132562049,-2.68935864031417,
6.94588888888888));
#19132=CARTESIAN_POINT('Ctrl Pts',(2.67339522049833,-0.825388609316905,
7.10375));
#19133=CARTESIAN_POINT('Ctrl Pts',(2.15357369271338,1.7861771220756,7.26161111111111));
#19134=CARTESIAN_POINT('Ctrl Pts',(-0.3168471224657,2.77991299546561,7.41947222222222));
#19135=CARTESIAN_POINT('Ctrl Pts',(-2.11399942046796,1.52539245310181,7.54940522121685));
#19136=CARTESIAN_POINT('Ctrl Pts',(-2.36856127073871,0.369714310321545,
7.62671784984111));
#19137=CARTESIAN_POINT('Ctrl Pts',(-2.36801892187683,0.000385579322849869,
7.65141010809499));
#19138=CARTESIAN_POINT('Ctrl Pts',(-2.36824488832617,0.000853070420097184,
6.84858989190503));
#19139=CARTESIAN_POINT('Ctrl Pts',(-2.36678180876479,-0.447463537758943,
6.87857025960238));
#19140=CARTESIAN_POINT('Ctrl Pts',(-2.02943011823198,-1.68535627820218,
6.96121559096642));
#19141=CARTESIAN_POINT('Ctrl Pts',(-0.0362940343214689,-2.79846637663312,
7.09652588599712));
#19142=CARTESIAN_POINT('Ctrl Pts',(2.32391314315961,-1.55953807940794,7.2545207769972));
#19143=CARTESIAN_POINT('Ctrl Pts',(2.57596499873257,1.09413693995685,7.41251566799723));
#19144=CARTESIAN_POINT('Ctrl Pts',(0.491210792034311,2.75525738831465,7.5705105589973));
#19145=CARTESIAN_POINT('Ctrl Pts',(-1.83676464589149,1.98397717256952,7.71586863363322));
#19146=CARTESIAN_POINT('Ctrl Pts',(-2.36622439910258,0.594323617306658,
7.80856174460247));
#19147=CARTESIAN_POINT('Ctrl Pts',(-2.37158591103805,-0.002113965830532,
7.84858989190503));
#19148=CARTESIAN_POINT('Origin',(0.,0.,-1.84858989190501));
#19149=CARTESIAN_POINT('',(-2.37251499866524,-0.00203510706959473,5.65141010809499));
#19150=CARTESIAN_POINT('',(-2.37459246787895,0.00132584644941116,5.84858989190502));
#19151=CARTESIAN_POINT('',(-2.37175,-2.62313128856983E-13,-1.84858989190501));
#19152=CARTESIAN_POINT('Ctrl Pts',(-2.37251499866524,-0.00203510706959476,
5.65141010809499));
#19153=CARTESIAN_POINT('Ctrl Pts',(-2.37392982983489,-0.158778764602934,
5.66194007206332));
#19154=CARTESIAN_POINT('Ctrl Pts',(-2.28863365792017,-1.09727074999648,
5.72509040640203));
#19155=CARTESIAN_POINT('Ctrl Pts',(-1.03894725747156,-2.59786392206505,
5.84086111111111));
#19156=CARTESIAN_POINT('Ctrl Pts',(1.60611030100396,-2.29100808867664,5.99872222222222));
#19157=CARTESIAN_POINT('Ctrl Pts',(2.79643351757374,0.090928230838667,6.15658333333333));
#19158=CARTESIAN_POINT('Ctrl Pts',(1.45388718569001,2.39050630885174,6.31444444444444));
#19159=CARTESIAN_POINT('Ctrl Pts',(-1.20551740739643,2.52488339173069,6.47230555555556));
#19160=CARTESIAN_POINT('Ctrl Pts',(-2.3208356274226,0.99330351170231,6.58462744343907));
#19161=CARTESIAN_POINT('Ctrl Pts',(-2.37479416424485,0.106880641648857,
6.64432896095221));
#19162=CARTESIAN_POINT('Ctrl Pts',(-2.37396076251026,0.00164080962999946,
6.65141010809499));
#19163=CARTESIAN_POINT('Ctrl Pts',(-2.37459246787895,0.00132584644941126,
5.84858989190502));
#19164=CARTESIAN_POINT('Ctrl Pts',(-2.3698592307678,-0.701510136856058,
5.8959138109356));
#19165=CARTESIAN_POINT('Ctrl Pts',(-1.6684907359976,-2.19471791424095,5.99590269363287));
#19166=CARTESIAN_POINT('Ctrl Pts',(0.864288593995119,-2.66190468356086,
6.14855653999681));
#19167=CARTESIAN_POINT('Ctrl Pts',(2.70163876039796,-0.730670463607777,
6.30655143099686));
#19168=CARTESIAN_POINT('Ctrl Pts',(2.08817696449889,1.86339697407977,6.46454632199692));
#19169=CARTESIAN_POINT('Ctrl Pts',(-0.419590302218696,2.76706980330411,
6.62254121299697));
#19170=CARTESIAN_POINT('Ctrl Pts',(-2.14308835195883,1.46541542002878,6.75055573629967));
#19171=CARTESIAN_POINT('Ctrl Pts',(-2.36935192507288,0.340071095547311,
6.82590529593569));
#19172=CARTESIAN_POINT('Ctrl Pts',(-2.36824488832617,0.000853070420097184,
6.84858989190503));
#19173=CARTESIAN_POINT('Origin',(0.,0.,-1.84858989190501));
#19174=CARTESIAN_POINT('',(-2.36803551809634,0.000435659979227324,4.65141010809499));
#19175=CARTESIAN_POINT('',(-2.37186713520955,-0.00210673407030348,4.84858989190502));
#19176=CARTESIAN_POINT('',(-2.37175,-2.62313128856983E-13,-1.84858989190501));
#19177=CARTESIAN_POINT('Ctrl Pts',(-2.36803551809634,0.000435659979227676,
4.65141010809499));
#19178=CARTESIAN_POINT('Ctrl Pts',(-2.36733685507668,-0.420470574046625,
4.67955118317444));
#19179=CARTESIAN_POINT('Ctrl Pts',(-2.06020439223756,-1.62937224150312,
4.76031262862425));
#19180=CARTESIAN_POINT('Ctrl Pts',(-0.135586668767159,-2.79462423533096,
4.89369444444444));
#19181=CARTESIAN_POINT('Ctrl Pts',(2.2650598786042,-1.64250178316317,5.05155555555556));
#19182=CARTESIAN_POINT('Ctrl Pts',(2.61412853009539,0.997316594419356,5.20941666666666));
#19183=CARTESIAN_POINT('Ctrl Pts',(0.595450368366912,2.73381550588105,5.36727777777778));
#19184=CARTESIAN_POINT('Ctrl Pts',(-1.79192767962886,2.0434990191552,5.51460892492054));
#19185=CARTESIAN_POINT('Ctrl Pts',(-2.36685963088812,0.624501153297232,
5.60931970169295));
#19186=CARTESIAN_POINT('Ctrl Pts',(-2.37251499866524,-0.00203510706959476,
5.65141010809499));
#19187=CARTESIAN_POINT('Ctrl Pts',(-2.37186713520955,-0.00210673407030307,
4.84858989190502));
#19188=CARTESIAN_POINT('Ctrl Pts',(-2.37348726775032,-0.180895246540068,
4.86059239860214));
#19189=CARTESIAN_POINT('Ctrl Pts',(-2.27367886126175,-1.14238681798702,
4.92525986896595));
#19190=CARTESIAN_POINT('Ctrl Pts',(-0.964512940920624,-2.62725067416123,
5.04259230299644));
#19191=CARTESIAN_POINT('Ctrl Pts',(1.67331967629405,-2.24337526486265,5.20058719399648));
#19192=CARTESIAN_POINT('Ctrl Pts',(2.79318773824162,0.175594923072764,5.35858208499656));
#19193=CARTESIAN_POINT('Ctrl Pts',(1.37919449268132,2.43527285317938,5.51657697599659));
#19194=CARTESIAN_POINT('Ctrl Pts',(-1.28594543116668,2.48577466117395,5.67457186699666));
#19195=CARTESIAN_POINT('Ctrl Pts',(-2.33566190719347,0.94159330950118,5.78524283896613));
#19196=CARTESIAN_POINT('Ctrl Pts',(-2.37512666773395,0.0806489125773547,
5.84324884726892));
#19197=CARTESIAN_POINT('Ctrl Pts',(-2.37459246787895,0.00132584644941126,
5.84858989190502));
#19198=CARTESIAN_POINT('Origin',(0.,0.,-1.84858989190501));
#19199=CARTESIAN_POINT('',(-2.37404189208837,0.00160568163382189,3.65141010809499));
#19200=CARTESIAN_POINT('',(-2.36815046112586,0.00071106261527204,3.84858989190502));
#19201=CARTESIAN_POINT('',(-2.37175,-2.62313128856983E-13,-1.84858989190501));
#19202=CARTESIAN_POINT('Ctrl Pts',(-2.37404189208837,0.0016056816338219,
3.65141010809499));
#19203=CARTESIAN_POINT('Ctrl Pts',(-2.36874097406567,-0.678301390146093,
3.69716229428555));
#19204=CARTESIAN_POINT('Ctrl Pts',(-1.70710264047504,-2.14919504149034,
3.79553485084648));
#19205=CARTESIAN_POINT('Ctrl Pts',(0.782578662553965,-2.68623882063674,
3.94652777777777));
#19206=CARTESIAN_POINT('Ctrl Pts',(2.67668699402767,-0.814650291328897,
4.10438888888889));
#19207=CARTESIAN_POINT('Ctrl Pts',(2.14638618582228,1.79480770611467,4.26225));
#19208=CARTESIAN_POINT('Ctrl Pts',(-0.328003825581952,2.77861869501174,
4.42011111111111));
#19209=CARTESIAN_POINT('Ctrl Pts',(-2.1171683957745,1.51896204170615,4.54983114714277));
#19210=CARTESIAN_POINT('Ctrl Pts',(-2.3686432695173,0.366572631058683,4.62693081280407));
#19211=CARTESIAN_POINT('Ctrl Pts',(-2.36803551809634,0.000435659979227676,
4.65141010809499));
#19212=CARTESIAN_POINT('Ctrl Pts',(-2.36815046112586,0.000711062615271901,
3.84858989190502));
#19213=CARTESIAN_POINT('Ctrl Pts',(-2.36695951468436,-0.438164069114789,
3.87793594993537));
#19214=CARTESIAN_POINT('Ctrl Pts',(-2.04015506879268,-1.66630099353556,
3.9599469716324));
#19215=CARTESIAN_POINT('Ctrl Pts',(-0.0697503817448946,-2.79783241149437,
4.09462295699612));
#19216=CARTESIAN_POINT('Ctrl Pts',(2.30510093209087,-1.58721170953314,4.25261784799616));
#19217=CARTESIAN_POINT('Ctrl Pts',(2.5888625630092,1.06326005653742,4.41061273899623));
#19218=CARTESIAN_POINT('Ctrl Pts',(0.524118009051023,2.74918744918107,4.56860762999628));
#19219=CARTESIAN_POINT('Ctrl Pts',(-1.82311086019465,2.00255204277458,4.71460001429921));
#19220=CARTESIAN_POINT('Ctrl Pts',(-2.36637840094874,0.603598422228309,
4.80792743493546));
#19221=CARTESIAN_POINT('Ctrl Pts',(-2.37186713520955,-0.00210673407030307,
4.84858989190502));
#19222=CARTESIAN_POINT('Origin',(0.,0.,-1.84858989190501));
#19223=CARTESIAN_POINT('',(-2.37242086931256,-0.00204814969984112,2.65141010809499));
#19224=CARTESIAN_POINT('',(-2.37437841508221,0.00145143062880153,2.84858989190502));
#19225=CARTESIAN_POINT('',(-2.37175,-2.62313128856983E-13,-1.84858989190501));
#19226=CARTESIAN_POINT('Ctrl Pts',(-2.37242086931256,-0.00204814969984169,
2.65141010809499));
#19227=CARTESIAN_POINT('Ctrl Pts',(-2.37386724785776,-0.161978223542019,
2.66215303502629));
#19228=CARTESIAN_POINT('Ctrl Pts',(-2.28652040521148,-1.10369798895945,
2.72551633232796));
#19229=CARTESIAN_POINT('Ctrl Pts',(-1.02851040967351,-2.60201352259292,
2.84149999999999));
#19230=CARTESIAN_POINT('Ctrl Pts',(1.61529402596567,-2.28454233775194,2.99936111111111));
#19231=CARTESIAN_POINT('Ctrl Pts',(2.79604598097933,0.102153087721166,3.15722222222222));
#19232=CARTESIAN_POINT('Ctrl Pts',(1.44427938842878,2.39632330140064,3.31508333333333));
#19233=CARTESIAN_POINT('Ctrl Pts',(-1.21564319790733,2.5200238088076,3.47294444444445));
#19234=CARTESIAN_POINT('Ctrl Pts',(-2.32270131739363,0.986891451715146,
3.58505336936499));
#19235=CARTESIAN_POINT('Ctrl Pts',(-2.37483765037521,0.103671339757588,
3.64454192391517));
#19236=CARTESIAN_POINT('Ctrl Pts',(-2.37404189208837,0.0016056816338219,
3.65141010809499));
#19237=CARTESIAN_POINT('Ctrl Pts',(-2.37437841508221,0.00145143062880148,
2.84858989190502));
#19238=CARTESIAN_POINT('Ctrl Pts',(-2.36936657242201,-0.69212851464997,
2.89527950126859));
#19239=CARTESIAN_POINT('Ctrl Pts',(-1.68411161328175,-2.17667922631145,
2.99463407429885));
#19240=CARTESIAN_POINT('Ctrl Pts',(0.832400628534772,-2.67204800324426,
3.1466536109958));
#19241=CARTESIAN_POINT('Ctrl Pts',(2.69270963387839,-0.762919488957052,
3.30464850199585));
#19242=CARTESIAN_POINT('Ctrl Pts',(2.11030679852043,1.83829718168443,3.4626433929959));
#19243=CARTESIAN_POINT('Ctrl Pts',(-0.386476751895552,2.77188871376435,
3.62063828399595));
#19244=CARTESIAN_POINT('Ctrl Pts',(-2.13403081733917,1.48458669705641,3.74928711696566));
#19245=CARTESIAN_POINT('Ctrl Pts',(-2.36909680859298,0.349449137499666,
3.82527098626868));
#19246=CARTESIAN_POINT('Ctrl Pts',(-2.36815046112586,0.000711062615271901,
3.84858989190502));
#19247=CARTESIAN_POINT('Origin',(0.,0.,-1.84858989190501));
#19248=CARTESIAN_POINT('',(-2.36805372255214,0.000487775483918624,1.65141010809499));
#19249=CARTESIAN_POINT('',(-2.37214954248261,-0.00208751672060303,1.84858989190502));
#19250=CARTESIAN_POINT('',(-2.37175,-2.62313128856983E-13,-1.84858989190501));
#19251=CARTESIAN_POINT('Ctrl Pts',(-2.36805372255214,0.000487775483918769,
1.65141010809499));
#19252=CARTESIAN_POINT('Ctrl Pts',(-2.36726911244657,-0.423596588857836,
1.6797641461374));
#19253=CARTESIAN_POINT('Ctrl Pts',(-2.0567282222087,-1.63578530702029,1.76073855455018));
#19254=CARTESIAN_POINT('Ctrl Pts',(-0.124366744542119,-2.79514315034066,
1.89433333333333));
#19255=CARTESIAN_POINT('Ctrl Pts',(2.27163476293377,-1.63339753074864,2.05219444444444));
#19256=CARTESIAN_POINT('Ctrl Pts',(2.61010413592219,1.00780309522069,2.21005555555555));
#19257=CARTESIAN_POINT('Ctrl Pts',(0.584471286669745,2.73618335546233,2.36791666666667));
#19258=CARTESIAN_POINT('Ctrl Pts',(-1.79666946585791,2.03730116384381,2.51503485084647));
#19259=CARTESIAN_POINT('Ctrl Pts',(-2.36678268187025,0.621381820955435,
2.60953266465592));
#19260=CARTESIAN_POINT('Ctrl Pts',(-2.37242086931256,-0.00204814969984169,
2.65141010809499));
#19261=CARTESIAN_POINT('Ctrl Pts',(-2.37214954248261,-0.00208751672060286,
1.84858989190502));
#19262=CARTESIAN_POINT('Ctrl Pts',(-2.37368814589582,-0.171375740131997,
1.85995808893514));
#19263=CARTESIAN_POINT('Ctrl Pts',(-2.28019409230745,-1.12323247312203,
1.92399124963194));
#19264=CARTESIAN_POINT('Ctrl Pts',(-0.995855715555496,-2.61553061219188,
2.04068937399542));
#19265=CARTESIAN_POINT('Ctrl Pts',(1.64637781974439,-2.26322161422709,2.19868426499547));
#19266=CARTESIAN_POINT('Ctrl Pts',(2.79508756969503,0.142186649832604,2.35667915599553));
#19267=CARTESIAN_POINT('Ctrl Pts',(1.40821242874264,2.41860884498944,2.51467404699558));
#19268=CARTESIAN_POINT('Ctrl Pts',(-1.25613315819632,2.50097199645567,2.67266893799564));
#19269=CARTESIAN_POINT('Ctrl Pts',(-2.33035893824447,0.960673681793537,
2.78397421963211));
#19270=CARTESIAN_POINT('Ctrl Pts',(-2.37501983264844,0.0902160608552179,
2.84261453760191));
#19271=CARTESIAN_POINT('Ctrl Pts',(-2.37437841508221,0.00145143062880148,
2.84858989190502));
#19272=CARTESIAN_POINT('Origin',(0.,0.,-1.84858989190501));
#19273=CARTESIAN_POINT('',(-2.37409249406917,0.00172857025301859,0.651410108094985));
#19274=CARTESIAN_POINT('',(-2.36806791026422,0.000580996437929415,0.848589891905023));
#19275=CARTESIAN_POINT('',(-2.37175,-2.62313128856983E-13,-1.84858989190501));
#19276=CARTESIAN_POINT('Ctrl Pts',(-2.37409249406917,0.00172857025301858,
0.651410108094986));
#19277=CARTESIAN_POINT('Ctrl Pts',(-2.36885059157359,-0.681255271864669,
0.697375257248508));
#19278=CARTESIAN_POINT('Ctrl Pts',(-1.70202128243095,-2.15553453151225,
0.7959607767724));
#19279=CARTESIAN_POINT('Ctrl Pts',(0.793380919254056,-2.68293732976497,
0.947166666666663));
#19280=CARTESIAN_POINT('Ctrl Pts',(2.67992237177449,-0.803971281251394,
1.10502777777777));
#19281=CARTESIAN_POINT('Ctrl Pts',(2.13917103413275,1.80344728451176,1.26288888888888));
#19282=CARTESIAN_POINT('Ctrl Pts',(-0.339158877291603,2.77725977180218,
1.42075));
#19283=CARTESIAN_POINT('Ctrl Pts',(-2.12031894951391,1.51253569372851,1.5502570730687));
#19284=CARTESIAN_POINT('Ctrl Pts',(-2.36872521807391,0.363433332120877,
1.62714377576703));
#19285=CARTESIAN_POINT('Ctrl Pts',(-2.36805372255214,0.000487775483918769,
1.65141010809499));
#19286=CARTESIAN_POINT('Ctrl Pts',(-2.36806791026422,0.000580996437929554,
0.848589891905023));
#19287=CARTESIAN_POINT('Ctrl Pts',(-2.36714590954407,-0.428850691797627,
0.877301640268363));
#19288=CARTESIAN_POINT('Ctrl Pts',(-2.05072593975983,-1.64725737587436,
0.958678352298389));
#19289=CARTESIAN_POINT('Ctrl Pts',(-0.103189861818606,-2.79677945469355,
1.0927200279951));
#19290=CARTESIAN_POINT('Ctrl Pts',(2.28595558559378,-1.6146683983646,1.25071491899515));
#19291=CARTESIAN_POINT('Ctrl Pts',(2.60139192527736,1.0322363870214,1.4087098099952));
#19292=CARTESIAN_POINT('Ctrl Pts',(0.556949311928898,2.7427217714679,1.56670470099526));
#19293=CARTESIAN_POINT('Ctrl Pts',(-1.80927361374524,2.02108563130788,1.7133313949652));
#19294=CARTESIAN_POINT('Ctrl Pts',(-2.36656032319539,0.612878624174093,
1.80729312526845));
#19295=CARTESIAN_POINT('Ctrl Pts',(-2.37214954248261,-0.00208751672060286,
1.84858989190502));
#19296=CARTESIAN_POINT('Origin',(0.,0.,15.5));
#19297=CARTESIAN_POINT('',(-2.86987326377042,0.00104132824445593,15.1339652973708));
#19298=CARTESIAN_POINT('Ctrl Pts',(-0.439445221994174,2.33068358199188,
15.62825));
#19299=CARTESIAN_POINT('Ctrl Pts',(-0.359491362851287,2.34930954683752,
15.6247606402091));
#19300=CARTESIAN_POINT('Ctrl Pts',(-0.27873128971825,2.36341107797762,15.6212855109979));
#19301=CARTESIAN_POINT('Ctrl Pts',(-0.197490043658781,2.37317361481181,
15.6178198845782));
#19302=CARTESIAN_POINT('Ctrl Pts',(-0.114097433923979,2.38319467509491,
15.6142624842978));
#19303=CARTESIAN_POINT('Ctrl Pts',(-0.0301970746788968,2.38864392614809,
15.610715096763));
#19304=CARTESIAN_POINT('Ctrl Pts',(0.0538748377108959,2.38966967391038,
15.6071726085593));
#19305=CARTESIAN_POINT('Ctrl Pts',(0.0936167287327529,2.39015455827456,
15.6054980281181));
#19306=CARTESIAN_POINT('Ctrl Pts',(0.133397101437596,2.38965022998153,15.6038245424699));
#19307=CARTESIAN_POINT('Ctrl Pts',(0.17318082101162,2.38816842541213,15.6021516114778));
#19308=CARTESIAN_POINT('Ctrl Pts',(0.19744268730314,2.38726475565179,15.601131384398));
#19309=CARTESIAN_POINT('Ctrl Pts',(0.221705799792773,2.38599750448324,15.6001113636003));
#19310=CARTESIAN_POINT('Ctrl Pts',(0.245962166148401,2.38436888753973,15.5990914265778));
#19311=CARTESIAN_POINT('Ctrl Pts',(0.26185491634123,2.38330181913124,15.5984231647255));
#19312=CARTESIAN_POINT('Ctrl Pts',(0.277745619245824,2.38207945021967,15.597754902985));
#19313=CARTESIAN_POINT('Ctrl Pts',(0.293615508622687,2.38070402970992,15.5970873017022));
#19314=CARTESIAN_POINT('Ctrl Pts',(0.379355905904818,2.37327303267301,15.5934804461119));
#19315=CARTESIAN_POINT('Ctrl Pts',(0.46460122999168,2.36137220783444,15.5898881158652));
#19316=CARTESIAN_POINT('Ctrl Pts',(0.548999070996607,2.3451645872232,15.5863050764217));
#19317=CARTESIAN_POINT('Ctrl Pts',(0.634137600151781,2.32881472609505,15.582690591685));
#19318=CARTESIAN_POINT('Ctrl Pts',(0.718414656351904,2.30808199543454,15.5790855615419));
#19319=CARTESIAN_POINT('Ctrl Pts',(0.801467682213623,2.28308069981211,15.5754846124216));
#19320=CARTESIAN_POINT('Ctrl Pts',(0.852459500288906,2.26773072905791,15.573273748452));
#19321=CARTESIAN_POINT('Ctrl Pts',(0.902989840792886,2.2507706713731,15.5710644228464));
#19322=CARTESIAN_POINT('Ctrl Pts',(0.952972256247749,2.23221757070223,15.5688553919549));
#19323=CARTESIAN_POINT('Ctrl Pts',(0.964785636442244,2.22783253188374,15.5683332858993));
#19324=CARTESIAN_POINT('Ctrl Pts',(0.976567164733754,2.22335887755768,15.5678112499871));
#19325=CARTESIAN_POINT('Ctrl Pts',(0.98830665315667,2.21880049805757,15.5672896716409));
#19326=CARTESIAN_POINT('Ctrl Pts',(1.07009362440554,2.18704306198486,15.5636559261431));
#19327=CARTESIAN_POINT('Ctrl Pts',(1.14996182974845,2.15113305037133,15.5600390318413));
#19328=CARTESIAN_POINT('Ctrl Pts',(1.22755227573139,2.11121890826833,15.5564336755567));
#19329=CARTESIAN_POINT('Ctrl Pts',(1.30476387614222,2.07149965222131,15.552845922899));
#19330=CARTESIAN_POINT('Ctrl Pts',(1.37972085381243,2.02781498993708,15.5492695958616));
#19331=CARTESIAN_POINT('Ctrl Pts',(1.45205674723287,1.98026157738062,15.5456994587133));
#19332=CARTESIAN_POINT('Ctrl Pts',(1.51163119176407,1.94109750537355,15.5427591627211));
#19333=CARTESIAN_POINT('Ctrl Pts',(1.56942781249227,1.89930836286272,15.5398230652386));
#19334=CARTESIAN_POINT('Ctrl Pts',(1.62522850219512,1.85492460083693,15.5368882414682));
#19335=CARTESIAN_POINT('Ctrl Pts',(1.65312884704655,1.83273271982404,15.5354208295831));
#19336=CARTESIAN_POINT('Ctrl Pts',(1.68052998038672,1.80989186082895,15.5339537361259));
#19337=CARTESIAN_POINT('Ctrl Pts',(1.70740302888556,1.78640394209333,15.532486595497));
#19338=CARTESIAN_POINT('Ctrl Pts',(1.72592667853778,1.77021366960761,15.5314752923321));
#19339=CARTESIAN_POINT('Ctrl Pts',(1.74419939199006,1.753715928893,15.5304639667541));
#19340=CARTESIAN_POINT('Ctrl Pts',(1.76221135665739,1.73691101229318,15.5294524990243));
#19341=CARTESIAN_POINT('Ctrl Pts',(1.77033011726031,1.72933631972932,15.528996587384));
#19342=CARTESIAN_POINT('Ctrl Pts',(1.77839409985328,1.72170084478485,15.5285407465195));
#19343=CARTESIAN_POINT('Ctrl Pts',(1.78639747681482,1.71400960641012,15.5280852527741));
#19344=CARTESIAN_POINT('Ctrl Pts',(1.84657495109044,1.65617910540199,15.5246603905846));
#19345=CARTESIAN_POINT('Ctrl Pts',(1.90341295390484,1.59512114682347,15.5212504095826));
#19346=CARTESIAN_POINT('Ctrl Pts',(1.95689046613085,1.53122773141625,15.5178508639384));
#19347=CARTESIAN_POINT('Ctrl Pts',(2.01194103421405,1.46545487347031,15.5143513197161));
#19348=CARTESIAN_POINT('Ctrl Pts',(2.06343093897923,1.39667671283205,15.5108628337987));
#19349=CARTESIAN_POINT('Ctrl Pts',(2.11130423046702,1.3252770563036,15.507380556377));
#19350=CARTESIAN_POINT('Ctrl Pts',(2.15745742078722,1.25644281002257,15.5040233981871));
#19351=CARTESIAN_POINT('Ctrl Pts',(2.20024928268006,1.18517117106803,15.500672010362));
#19352=CARTESIAN_POINT('Ctrl Pts',(2.23959635988792,1.11177753196584,15.4973220472993));
#19353=CARTESIAN_POINT('Ctrl Pts',(2.25681070616636,1.07966781485864,15.4958564384594));
#19354=CARTESIAN_POINT('Ctrl Pts',(2.27336525378777,1.04715163497876,15.4943911023279));
#19355=CARTESIAN_POINT('Ctrl Pts',(2.28925084670373,1.0142542353915,15.4929256750031));
#19356=CARTESIAN_POINT('Ctrl Pts',(2.29885484868501,0.994365352899876,15.4920397170785));
#19357=CARTESIAN_POINT('Ctrl Pts',(2.30821431569525,0.974337119524171,15.491153725822));
#19358=CARTESIAN_POINT('Ctrl Pts',(2.3173269757796,0.954175024263046,15.4902676208197));
#19359=CARTESIAN_POINT('Ctrl Pts',(2.32227232757467,0.943233251710468,15.4897867402729));
#19360=CARTESIAN_POINT('Ctrl Pts',(2.32714420559321,0.932253683866113,15.4893058986854));
#19361=CARTESIAN_POINT('Ctrl Pts',(2.33193873109372,0.921245710398884,15.4888254510349));
#19362=CARTESIAN_POINT('Ctrl Pts',(2.36754247444614,0.839501424730483,15.4852576871677));
#19363=CARTESIAN_POINT('Ctrl Pts',(2.39894281260828,0.756064329075142,15.4817059560376));
#19364=CARTESIAN_POINT('Ctrl Pts',(2.42608268559146,0.671340103595013,15.4781652340513));
#19365=CARTESIAN_POINT('Ctrl Pts',(2.453534139292,0.58564319725637,15.4745838626229));
#19366=CARTESIAN_POINT('Ctrl Pts',(2.47662715562456,0.498628540954889,15.4710137545713));
#19367=CARTESIAN_POINT('Ctrl Pts',(2.49525785992387,0.410687466692489,15.4674497112883));
#19368=CARTESIAN_POINT('Ctrl Pts',(2.51258257274376,0.328910963121187,15.4641355034428));
#19369=CARTESIAN_POINT('Ctrl Pts',(2.52604844140045,0.24633247953868,15.4608265399003));
#19370=CARTESIAN_POINT('Ctrl Pts',(2.53553303361489,0.163255416668028,15.4575186404574));
#19371=CARTESIAN_POINT('Ctrl Pts',(2.53942998139287,0.129121426694033,15.4561595191486));
#19372=CARTESIAN_POINT('Ctrl Pts',(2.54265436806282,0.0949032017028567,
15.4548005774761));
#19373=CARTESIAN_POINT('Ctrl Pts',(2.54519570834653,0.0606216731012661,
15.4534415254952));
#19374=CARTESIAN_POINT('Ctrl Pts',(2.54650804671318,0.0429188233335401,
15.4527397162695));
#19375=CARTESIAN_POINT('Ctrl Pts',(2.5476382209856,0.0251990932110098,15.4520378776284));
#19376=CARTESIAN_POINT('Ctrl Pts',(2.54858465973821,0.00746537430393359,
15.4513359696452));
#19377=CARTESIAN_POINT('Ctrl Pts',(2.54936740774304,-0.00720121986763361,
15.4507554597369));
#19378=CARTESIAN_POINT('Ctrl Pts',(2.55002444266908,-0.0218786230829287,
15.4501748534934));
#19379=CARTESIAN_POINT('Ctrl Pts',(2.55055443165925,-0.0365475000712079,
15.4495948274855));
#19380=CARTESIAN_POINT('Ctrl Pts',(2.55387898415761,-0.128563471239416,
15.4459563992365));
#19381=CARTESIAN_POINT('Ctrl Pts',(2.55221836548087,-0.22040066645441,15.4423345418383));
#19382=CARTESIAN_POINT('Ctrl Pts',(2.5454697064449,-0.311650010793409,15.4387239299593));
#19383=CARTESIAN_POINT('Ctrl Pts',(2.53872104740894,-0.402899355132408,
15.4351133180804));
#19384=CARTESIAN_POINT('Ctrl Pts',(2.52688470709894,-0.49356189746232,15.4315139517205));
#19385=CARTESIAN_POINT('Ctrl Pts',(2.50980235603637,-0.583236219097685,
15.4279205055482));
#19386=CARTESIAN_POINT('Ctrl Pts',(2.49326213150481,-0.670064631014266,
15.424441101202));
#19387=CARTESIAN_POINT('Ctrl Pts',(2.47180332144007,-0.755967381987536,
15.420967247239));
#19388=CARTESIAN_POINT('Ctrl Pts',(2.44569482135312,-0.840684658565203,
15.4174941094224));
#19389=CARTESIAN_POINT('Ctrl Pts',(2.43658807165331,-0.870234384917672,
15.4162826650015));
#19390=CARTESIAN_POINT('Ctrl Pts',(2.42691516765274,-0.899639766052948,
15.41507130771));
#19391=CARTESIAN_POINT('Ctrl Pts',(2.41668612527745,-0.928889320342703,
15.4138598323975));
#19392=CARTESIAN_POINT('Ctrl Pts',(2.41079789512425,-0.945726488595391,
15.4131624606198));
#19393=CARTESIAN_POINT('Ctrl Pts',(2.40472537046329,-0.962512016907764,
15.4124650497348));
#19394=CARTESIAN_POINT('Ctrl Pts',(2.39847036187175,-0.979243667871416,
15.4117675606113));
#19395=CARTESIAN_POINT('Ctrl Pts',(2.39421301098727,-0.990631743201221,
15.4112928281));
#19396=CARTESIAN_POINT('Ctrl Pts',(2.38987156242605,-1.0019935463669,15.4108181134517));
#19397=CARTESIAN_POINT('Ctrl Pts',(2.38545028303317,-1.01331939423191,15.4103437824454));
#19398=CARTESIAN_POINT('Ctrl Pts',(2.35279097735238,-1.09698167717045,15.4068399728119));
#19399=CARTESIAN_POINT('Ctrl Pts',(2.31572987674733,-1.17881857921774,15.4033514296728));
#19400=CARTESIAN_POINT('Ctrl Pts',(2.27459874133947,-1.25857844945699,15.3998733992833));
#19401=CARTESIAN_POINT('Ctrl Pts',(2.23281288372258,-1.33960793109688,15.396340005877));
#19402=CARTESIAN_POINT('Ctrl Pts',(2.18682594253521,-1.41849449977561,15.3928174625663));
#19403=CARTESIAN_POINT('Ctrl Pts',(2.13693151879332,-1.49496175096055,15.3893007849646));
#19404=CARTESIAN_POINT('Ctrl Pts',(2.08679723793274,-1.57179660263405,15.385767201663));
#19405=CARTESIAN_POINT('Ctrl Pts',(2.03271725897117,-1.64618961960946,15.3822395406022));
#19406=CARTESIAN_POINT('Ctrl Pts',(1.97494281786374,-1.71783598585985,15.3787127451654));
#19407=CARTESIAN_POINT('Ctrl Pts',(1.95216878512211,-1.74607817495815,15.3773225222016));
#19408=CARTESIAN_POINT('Ctrl Pts',(1.92882022676702,-1.77389324483966,15.3759324337425));
#19409=CARTESIAN_POINT('Ctrl Pts',(1.90491084697345,-1.80126106485015,15.3745421700657));
#19410=CARTESIAN_POINT('Ctrl Pts',(1.89303589564547,-1.8148537022746,15.3738516748025));
#19411=CARTESIAN_POINT('Ctrl Pts',(1.88102258946071,-1.82833599951471,15.3731611363172));
#19412=CARTESIAN_POINT('Ctrl Pts',(1.86887253021617,-1.84170540057035,15.3724705166642));
#19413=CARTESIAN_POINT('Ctrl Pts',(1.86055716973053,-1.85085526453538,15.3719978645349));
#19414=CARTESIAN_POINT('Ctrl Pts',(1.8521789913077,-1.85995082597714,15.3715252464369));
#19415=CARTESIAN_POINT('Ctrl Pts',(1.84374494253208,-1.86898463564396,15.3710530027583));
#19416=CARTESIAN_POINT('Ctrl Pts',(1.77862481272331,-1.93873557897155,15.3674067623267));
#19417=CARTESIAN_POINT('Ctrl Pts',(1.71007452953627,-2.00492197279666,15.3637769310107));
#19418=CARTESIAN_POINT('Ctrl Pts',(1.63841756617314,-2.06724394639147,15.3601581531957));
#19419=CARTESIAN_POINT('Ctrl Pts',(1.56864469297252,-2.1279272764847,15.3566345245939));
#19420=CARTESIAN_POINT('Ctrl Pts',(1.49592552744324,-2.18494739655425,15.3531213758712));
#19421=CARTESIAN_POINT('Ctrl Pts',(1.42051657448793,-2.237996979208,15.3496137628515));
#19422=CARTESIAN_POINT('Ctrl Pts',(1.34626553575621,-2.29023197866037,15.3461600096832));
#19423=CARTESIAN_POINT('Ctrl Pts',(1.26940602418092,-2.33861808827242,15.3427116235202));
#19424=CARTESIAN_POINT('Ctrl Pts',(1.19015227451303,-2.38282228508801,15.3392638844625));
#19425=CARTESIAN_POINT('Ctrl Pts',(1.16438136391748,-2.39719614637352,15.3381427845096));
#19426=CARTESIAN_POINT('Ctrl Pts',(1.1383570943619,-2.4111274748391,15.3370217529787));
#19427=CARTESIAN_POINT('Ctrl Pts',(1.11208629310672,-2.42460372067378,15.3359006275904));
#19428=CARTESIAN_POINT('Ctrl Pts',(1.09252404263768,-2.4346386523776,15.3350657944447));
#19429=CARTESIAN_POINT('Ctrl Pts',(1.07282508844486,-2.44442123549769,15.3342309092564));
#19430=CARTESIAN_POINT('Ctrl Pts',(1.05299217133848,-2.4539460706498,15.3333959050218));
#19431=CARTESIAN_POINT('Ctrl Pts',(1.04038456497523,-2.46000092237074,15.3328651003678));
#19432=CARTESIAN_POINT('Ctrl Pts',(1.02772285622574,-2.46595150778408,15.3323342505181));
#19433=CARTESIAN_POINT('Ctrl Pts',(1.01502087310116,-2.47179063085649,15.3318038822616));
#19434=CARTESIAN_POINT('Ctrl Pts',(0.982652722257195,-2.48667032440912,
15.3304523578927));
#19435=CARTESIAN_POINT('Ctrl Pts',(0.950002091670773,-2.50083650005249,
15.3291030741213));
#19436=CARTESIAN_POINT('Ctrl Pts',(0.917084170499721,-2.5142729570447,15.3277557583224));
#19437=CARTESIAN_POINT('Ctrl Pts',(0.834495683370104,-2.5479839757206,15.3243754484619));
#19438=CARTESIAN_POINT('Ctrl Pts',(0.750226663082229,-2.57710500546031,
15.3210075263739));
#19439=CARTESIAN_POINT('Ctrl Pts',(0.664646844355562,-2.60177034865307,
15.317647686521));
#19440=CARTESIAN_POINT('Ctrl Pts',(0.576787650214132,-2.6270926408521,15.3141983590239));
#19441=CARTESIAN_POINT('Ctrl Pts',(0.487546169865586,-2.64771888106776,
15.3107575500279));
#19442=CARTESIAN_POINT('Ctrl Pts',(0.397298853288816,-2.66374516605354,
15.3073206007236));
#19443=CARTESIAN_POINT('Ctrl Pts',(0.308910977458226,-2.67944124812091,
15.3039544657529));
#19444=CARTESIAN_POINT('Ctrl Pts',(0.219557440695963,-2.69072476824651,
15.3005920330634));
#19445=CARTESIAN_POINT('Ctrl Pts',(0.129581594551193,-2.69764046998944,
15.2972289259214));
#19446=CARTESIAN_POINT('Ctrl Pts',(0.0974227261046785,-2.7001122571645,
15.2960268953233));
#19447=CARTESIAN_POINT('Ctrl Pts',(0.0651843226484069,-2.70202565483482,
15.2948247785662));
#19448=CARTESIAN_POINT('Ctrl Pts',(0.0328820436324132,-2.7033813247538,
15.2936223758136));
#19449=CARTESIAN_POINT('Ctrl Pts',(0.0192199250543532,-2.70395469987624,
15.2931138244208));
#19450=CARTESIAN_POINT('Ctrl Pts',(0.00555605037576419,-2.70442788901379,
15.2926055817652));
#19451=CARTESIAN_POINT('Ctrl Pts',(-0.00810768527292701,-2.70480131817288,
15.2920976575977));
#19452=CARTESIAN_POINT('Ctrl Pts',(-0.102177189495074,-2.70737223265483,
15.2886007973064));
#19453=CARTESIAN_POINT('Ctrl Pts',(-0.196248953232544,-2.705219350857,15.2851186519246));
#19454=CARTESIAN_POINT('Ctrl Pts',(-0.28992790026966,-2.69846111693802,
15.2816464960614));
#19455=CARTESIAN_POINT('Ctrl Pts',(-0.384721183626751,-2.69162249200534,
15.2781330379685));
#19456=CARTESIAN_POINT('Ctrl Pts',(-0.479113197863739,-2.68006831395088,
15.2746298084638));
#19457=CARTESIAN_POINT('Ctrl Pts',(-0.572703609774366,-2.66386867615587,
15.2711319115131));
#19458=CARTESIAN_POINT('Ctrl Pts',(-0.670406973022026,-2.64695712438838,
15.2674802949704));
#19459=CARTESIAN_POINT('Ctrl Pts',(-0.767237930320469,-2.62498318167097,
15.2638344899723));
#19460=CARTESIAN_POINT('Ctrl Pts',(-0.862734200133818,-2.5979664405403,
15.2601889262148));
#19461=CARTESIAN_POINT('Ctrl Pts',(-0.899309423475345,-2.58761898568426,
15.258792669493));
#19462=CARTESIAN_POINT('Ctrl Pts',(-0.935688693950487,-2.57653116703875,
15.2573964481588));
#19463=CARTESIAN_POINT('Ctrl Pts',(-0.971845190453781,-2.56470173355219,
15.2559999492582));
#19464=CARTESIAN_POINT('Ctrl Pts',(-0.985718422450195,-2.56016278506391,
15.2554641132369));
#19465=CARTESIAN_POINT('Ctrl Pts',(-0.999558849945709,-2.55551463851664,
15.2549282363508));
#19466=CARTESIAN_POINT('Ctrl Pts',(-1.01336493152648,-2.55075717270086,
15.254392300921));
#19467=CARTESIAN_POINT('Ctrl Pts',(-1.02713823497804,-2.5460110019675,15.2538576378986));
#19468=CARTESIAN_POINT('Ctrl Pts',(-1.0408680078023,-2.54115923920241,15.2533232792799));
#19469=CARTESIAN_POINT('Ctrl Pts',(-1.05455083068562,-2.53620294641156,
15.2527892870021));
#19470=CARTESIAN_POINT('Ctrl Pts',(-1.14480706402235,-2.50350966941525,
15.2492669048126));
#19471=CARTESIAN_POINT('Ctrl Pts',(-1.23304972084596,-2.46626241239109,
15.2457593395817));
#19472=CARTESIAN_POINT('Ctrl Pts',(-1.3188786706842,-2.42453542284507,15.242261762893));
#19473=CARTESIAN_POINT('Ctrl Pts',(-1.40341018907482,-2.38343919842613,
15.238817057246));
#19474=CARTESIAN_POINT('Ctrl Pts',(-1.48560133565556,-2.33799743942912,
15.2353820404405));
#19475=CARTESIAN_POINT('Ctrl Pts',(-1.56505752288372,-2.28823266258407,
15.2319520997326));
#19476=CARTESIAN_POINT('Ctrl Pts',(-1.59875150777533,-2.26712954025155,
15.2304976079627));
#19477=CARTESIAN_POINT('Ctrl Pts',(-1.63195344745741,-2.24524844976825,
15.2290440290004));
#19478=CARTESIAN_POINT('Ctrl Pts',(-1.66463195977674,-2.22258855435451,
15.2275910110965));
#19479=CARTESIAN_POINT('Ctrl Pts',(-1.74176819837999,-2.16910083489293,
15.2241612241271));
#19480=CARTESIAN_POINT('Ctrl Pts',(-1.81599039866318,-2.11127647963352,
15.2207345632396));
#19481=CARTESIAN_POINT('Ctrl Pts',(-1.88715256813859,-2.04946422501414,
15.2173064022613));
#19482=CARTESIAN_POINT('Ctrl Pts',(-1.90164577925548,-2.03687526008497,
15.2166082074035));
#19483=CARTESIAN_POINT('Ctrl Pts',(-1.91601194648249,-2.02412075255685,
15.215909950323));
#19484=CARTESIAN_POINT('Ctrl Pts',(-1.9302496520377,-2.01120346334021,15.2152115919387));
#19485=CARTESIAN_POINT('Ctrl Pts',(-1.94128816753001,-2.0011886687103,15.2146701535858));
#19486=CARTESIAN_POINT('Ctrl Pts',(-1.95224352654855,-1.99108137253609,
15.2141289446068));
#19487=CARTESIAN_POINT('Ctrl Pts',(-1.96311133771197,-1.98088698275119,
15.2135881466736));
#19488=CARTESIAN_POINT('Ctrl Pts',(-2.03178675603926,-1.91646702066845,
15.2101707589647));
#19489=CARTESIAN_POINT('Ctrl Pts',(-2.09701995613675,-1.8485265277173,15.2067672577273));
#19490=CARTESIAN_POINT('Ctrl Pts',(-2.15871310631003,-1.77747212767664,
15.2033732357386));
#19491=CARTESIAN_POINT('Ctrl Pts',(-2.22164945390415,-1.7049858888237,15.1999108197811));
#19492=CARTESIAN_POINT('Ctrl Pts',(-2.28090217022322,-1.62925832538052,
15.19645826896));
#19493=CARTESIAN_POINT('Ctrl Pts',(-2.33633512040192,-1.55067589533689,
15.1930109042136));
#19494=CARTESIAN_POINT('Ctrl Pts',(-2.39218601791983,-1.47150097801918,
15.1895375474008));
#19495=CARTESIAN_POINT('Ctrl Pts',(-2.44415984798534,-1.38942718616138,
15.1860694551604));
#19496=CARTESIAN_POINT('Ctrl Pts',(-2.49207710040016,-1.30481547317471,
15.1826018417945));
#19497=CARTESIAN_POINT('Ctrl Pts',(-2.52022211747796,-1.25511733759765,
15.1805650798249));
#19498=CARTESIAN_POINT('Ctrl Pts',(-2.54696681998739,-1.20454303320315,
15.1785284830672));
#19499=CARTESIAN_POINT('Ctrl Pts',(-2.57226731600719,-1.15316195438398,
15.1764910817393));
#19500=CARTESIAN_POINT('Ctrl Pts',(-2.57933924906923,-1.13880004030214,
15.1759215922795));
#19501=CARTESIAN_POINT('Ctrl Pts',(-2.58629893239321,-1.12437358425022,
15.1753519825172));
#19502=CARTESIAN_POINT('Ctrl Pts',(-2.59313735551554,-1.10990147500019,
15.1747829112963));
#19503=CARTESIAN_POINT('Ctrl Pts',(-2.63517066423893,-1.02094666405867,
15.1712850367298));
#19504=CARTESIAN_POINT('Ctrl Pts',(-2.6726976453638,-0.930127060905838,
15.167801819036));
#19505=CARTESIAN_POINT('Ctrl Pts',(-2.70558302354023,-0.837840896222647,
15.1643285389057));
#19506=CARTESIAN_POINT('Ctrl Pts',(-2.73847376195491,-0.745539689114618,
15.1608546926391));
#19507=CARTESIAN_POINT('Ctrl Pts',(-2.76672184052432,-0.651770570287676,
15.1573907871758));
#19508=CARTESIAN_POINT('Ctrl Pts',(-2.79014819101862,-0.556903769359717,
15.1539321008988));
#19509=CARTESIAN_POINT('Ctrl Pts',(-2.81305355218475,-0.464146754627161,
15.1505503339286));
#19510=CARTESIAN_POINT('Ctrl Pts',(-2.83134952927604,-0.370339481518358,
15.1471735565822));
#19511=CARTESIAN_POINT('Ctrl Pts',(-2.8448219024633,-0.275813943398833,
15.1437973553073));
#19512=CARTESIAN_POINT('Ctrl Pts',(-2.85447686455589,-0.208072315799913,
15.1413778042102));
#19513=CARTESIAN_POINT('Ctrl Pts',(-2.86165354894421,-0.139961477196466,
15.1389585489751));
#19514=CARTESIAN_POINT('Ctrl Pts',(-2.86625656775569,-0.071602632167948,
15.1365379651471));
#19515=CARTESIAN_POINT('Ctrl Pts',(-2.8678889837078,-0.0473598311579388,
15.1356795285827));
#19516=CARTESIAN_POINT('Ctrl Pts',(-2.86919553394546,-0.0231160969724086,
15.1348219958471));
#19517=CARTESIAN_POINT('Ctrl Pts',(-2.87017396612668,0.00112290304428943,
15.1339652973708));
#19518=CARTESIAN_POINT('',(0.261080338132197,2.92584241055005,15.058));
#19519=CARTESIAN_POINT('Ctrl Pts',(0.260984867623723,2.92515103163649,15.058));
#19520=CARTESIAN_POINT('Ctrl Pts',(0.163110290089364,2.92129299518303,15.0703787026841));
#19521=CARTESIAN_POINT('Ctrl Pts',(0.0656985383021158,2.91278590387498,
15.0828015605825));
#19522=CARTESIAN_POINT('Ctrl Pts',(-0.0308724856851826,2.89964343902045,
15.0952881213498));
#19523=CARTESIAN_POINT('Ctrl Pts',(-0.13093434020212,2.88602590291106,15.1082260438789));
#19524=CARTESIAN_POINT('Ctrl Pts',(-0.230094798512676,2.86743186329655,
15.121232357953));
#19525=CARTESIAN_POINT('Ctrl Pts',(-0.327908726704405,2.84382209488468,
15.1343288085909));
#19526=CARTESIAN_POINT('Ctrl Pts',(-0.401269172848201,2.82611476857578,
15.1441511465694));
#19527=CARTESIAN_POINT('Ctrl Pts',(-0.473871776581697,2.80558493098147,
15.154024186365));
#19528=CARTESIAN_POINT('Ctrl Pts',(-0.54551386023679,2.78219703023119,15.1639571016578));
#19529=CARTESIAN_POINT('Ctrl Pts',(-0.599245422978111,2.76465610466849,
15.1714067881273));
#19530=CARTESIAN_POINT('Ctrl Pts',(-0.652436445713434,2.74550717996222,
15.178890154564));
#19531=CARTESIAN_POINT('Ctrl Pts',(-0.704995275147146,2.7247296345796,15.186411071114));
#19532=CARTESIAN_POINT('Ctrl Pts',(-0.720729468886594,2.71850959642421,
15.1886625588158));
#19533=CARTESIAN_POINT('Ctrl Pts',(-0.736406966678059,2.71214357207348,
15.1909174117022));
#19534=CARTESIAN_POINT('Ctrl Pts',(-0.752025204049111,2.70563092815761,
15.1931757336031));
#19535=CARTESIAN_POINT('Ctrl Pts',(-0.764775912501757,2.70031401422844,
15.1950194246335));
#19536=CARTESIAN_POINT('Ctrl Pts',(-0.777478081511626,2.69490314594757,
15.196864120682));
#19537=CARTESIAN_POINT('Ctrl Pts',(-0.790130440968904,2.6893983882733,15.1987098648068));
#19538=CARTESIAN_POINT('Ctrl Pts',(-0.873485337988913,2.65313254310755,
15.2108697952897));
#19539=CARTESIAN_POINT('Ctrl Pts',(-0.954683148186728,2.61279395749136,
15.2230755503321));
#19540=CARTESIAN_POINT('Ctrl Pts',(-1.0333900295422,2.56835839969231,15.2353460721376));
#19541=CARTESIAN_POINT('Ctrl Pts',(-1.07474974365993,2.54500793864519,15.2417941141031));
#19542=CARTESIAN_POINT('Ctrl Pts',(-1.11542111238663,2.52052546068703,15.2482600407761));
#19543=CARTESIAN_POINT('Ctrl Pts',(-1.15535178122673,2.49490314259947,15.2547466008415));
#19544=CARTESIAN_POINT('Ctrl Pts',(-1.23327915249916,2.44489947493076,15.2674055567063));
#19545=CARTESIAN_POINT('Ctrl Pts',(-1.30838829429154,2.39055588937394,15.2801430971848));
#19546=CARTESIAN_POINT('Ctrl Pts',(-1.38046450469962,2.33219918561456,15.2929796526032));
#19547=CARTESIAN_POINT('Ctrl Pts',(-1.45426350057602,2.27244762382022,15.3061230309111));
#19548=CARTESIAN_POINT('Ctrl Pts',(-1.52488347180723,2.20848778279982,15.3193702140928));
#19549=CARTESIAN_POINT('Ctrl Pts',(-1.59204074405781,2.14065188994946,15.332743132764));
#19550=CARTESIAN_POINT('Ctrl Pts',(-1.60237109058904,2.13021715582588,15.3348001979094));
#19551=CARTESIAN_POINT('Ctrl Pts',(-1.61262065491134,2.1196893711682,15.3368604944486));
#19552=CARTESIAN_POINT('Ctrl Pts',(-1.62278430900332,2.10907388768773,15.3389232952054));
#19553=CARTESIAN_POINT('Ctrl Pts',(-1.68486768809848,2.04423056665054,15.3515236493914));
#19554=CARTESIAN_POINT('Ctrl Pts',(-1.74353795945352,1.97633977637267,15.3641743680265));
#19555=CARTESIAN_POINT('Ctrl Pts',(-1.79863355499942,1.90572574364455,15.3768970731667));
#19556=CARTESIAN_POINT('Ctrl Pts',(-1.8536060338742,1.83526950510231,15.3895913481376));
#19557=CARTESIAN_POINT('Ctrl Pts',(-1.90502010402237,1.76210117952091,15.4023572882508));
#19558=CARTESIAN_POINT('Ctrl Pts',(-1.95266740197694,1.68652354076833,15.4152163709358));
#19559=CARTESIAN_POINT('Ctrl Pts',(-1.999553014057,1.61215408007279,15.4278698893587));
#19560=CARTESIAN_POINT('Ctrl Pts',(-2.04279147033365,1.53545080587127,15.4406135962167));
#19561=CARTESIAN_POINT('Ctrl Pts',(-2.08213462636226,1.45669772176484,15.4534679553077));
#19562=CARTESIAN_POINT('Ctrl Pts',(-2.10370638024081,1.41351760306046,15.4605159681915));
#19563=CARTESIAN_POINT('Ctrl Pts',(-2.12410620181193,1.36972125073741,15.4675972464718));
#19564=CARTESIAN_POINT('Ctrl Pts',(-2.14328646703913,1.32535636167276,15.4747151632939));
#19565=CARTESIAN_POINT('Ctrl Pts',(-2.15012579550102,1.30953666132481,15.4772532810172));
#19566=CARTESIAN_POINT('Ctrl Pts',(-2.15681001155505,1.29364468163272,15.4797960573454));
#19567=CARTESIAN_POINT('Ctrl Pts',(-2.16333680365848,1.27768262506038,15.4823436452153));
#19568=CARTESIAN_POINT('Ctrl Pts',(-2.16791412260327,1.2664882400105,15.4841302996752));
#19569=CARTESIAN_POINT('Ctrl Pts',(-2.17241292255598,1.25526195256421,15.4859189101699));
#19570=CARTESIAN_POINT('Ctrl Pts',(-2.17682958710993,1.24401228867859,15.4877083034276));
#19571=CARTESIAN_POINT('Ctrl Pts',(-2.20791015801245,1.16484712416239,15.5003004673422));
#19572=CARTESIAN_POINT('Ctrl Pts',(-2.2349734122897,1.08441291813616,15.5129492481641));
#19573=CARTESIAN_POINT('Ctrl Pts',(-2.25783961089921,1.00297802743715,15.5256767231474));
#19574=CARTESIAN_POINT('Ctrl Pts',(-2.28035828534265,0.922780797311416,
15.5382107639178));
#19575=CARTESIAN_POINT('Ctrl Pts',(-2.29880657051476,0.841612257746407,
15.5508211250137));
#19576=CARTESIAN_POINT('Ctrl Pts',(-2.31296316132111,0.759731453145844,
15.5635288923091));
#19577=CARTESIAN_POINT('Ctrl Pts',(-2.32670958827523,0.680223009708963,
15.5758684730222));
#19578=CARTESIAN_POINT('Ctrl Pts',(-2.33640931253598,0.600042348520933,
15.5882998973352));
#19579=CARTESIAN_POINT('Ctrl Pts',(-2.34181299591968,0.519439649300842,
15.6008424709262));
#19580=CARTESIAN_POINT('Ctrl Pts',(-2.34572284670801,0.461119332452094,
15.609917686434));
#19581=CARTESIAN_POINT('Ctrl Pts',(-2.34738263953658,0.402578305857885,
15.6190510917899));
#19582=CARTESIAN_POINT('Ctrl Pts',(-2.34668236863854,0.343918483395394,
15.62825));
#19583=CARTESIAN_POINT('',(-2.14373220034752,2.0119373894844,15.058));
#19584=CARTESIAN_POINT('Origin',(0.,0.,15.058));
#19585=CARTESIAN_POINT('Ctrl Pts',(-2.87017396612668,0.00112290304428943,
15.1339652973708));
#19586=CARTESIAN_POINT('Ctrl Pts',(-2.87266912500978,0.0629362380616879,
15.1317805789463));
#19587=CARTESIAN_POINT('Ctrl Pts',(-2.87303098230106,0.124718621761705,
15.1296012856735));
#19588=CARTESIAN_POINT('Ctrl Pts',(-2.87121685856479,0.18637804904607,15.1274262638706));
#19589=CARTESIAN_POINT('Ctrl Pts',(-2.86841400163638,0.281643079490827,
15.1240658123162));
#19590=CARTESIAN_POINT('Ctrl Pts',(-2.86041988710444,0.376614623554742,
15.1207155571276));
#19591=CARTESIAN_POINT('Ctrl Pts',(-2.84750858059062,0.47099184224787,15.1173712434175));
#19592=CARTESIAN_POINT('Ctrl Pts',(-2.83433033308302,0.567320307975548,
15.1139577860911));
#19593=CARTESIAN_POINT('Ctrl Pts',(-2.81602924148459,0.663030385704492,
15.1105505184628));
#19594=CARTESIAN_POINT('Ctrl Pts',(-2.79284156103339,0.757800921120369,
15.1071449162423));
#19595=CARTESIAN_POINT('Ctrl Pts',(-2.77879319434313,0.815218101582043,
15.1050816159094));
#19596=CARTESIAN_POINT('Ctrl Pts',(-2.76295010551778,0.872290339259573,
15.1030189268812));
#19597=CARTESIAN_POINT('Ctrl Pts',(-2.74535586092349,0.928944130664371,
15.100955843023));
#19598=CARTESIAN_POINT('Ctrl Pts',(-2.7354097693855,0.960970728468381,15.099789574088));
#19599=CARTESIAN_POINT('Ctrl Pts',(-2.72490394590206,0.992863566804536,
15.098623178978));
#19600=CARTESIAN_POINT('Ctrl Pts',(-2.7138453785436,1.0246089965303,15.0974564759315));
#19601=CARTESIAN_POINT('Ctrl Pts',(-2.70868377697821,1.03942621963478,15.0969119156755));
#19602=CARTESIAN_POINT('Ctrl Pts',(-2.7034040983514,1.05420445638712,15.0963675402945));
#19603=CARTESIAN_POINT('Ctrl Pts',(-2.69801003661965,1.06893536837389,15.0958235919881));
#19604=CARTESIAN_POINT('Ctrl Pts',(-2.66394262772994,1.16197175299988,15.0923881642358));
#19605=CARTESIAN_POINT('Ctrl Pts',(-2.62528653689294,1.25320878716493,15.0889665364856));
#19606=CARTESIAN_POINT('Ctrl Pts',(-2.58232115247044,1.34232723597939,15.0855542358814));
#19607=CARTESIAN_POINT('Ctrl Pts',(-2.53887733631532,1.43243804397901,15.0821039383428));
#19608=CARTESIAN_POINT('Ctrl Pts',(-2.49102735184572,1.52038366982231,15.0786631768276));
#19609=CARTESIAN_POINT('Ctrl Pts',(-2.43900735397324,1.60582293428401,15.0752273273902));
#19610=CARTESIAN_POINT('Ctrl Pts',(-2.38725398360023,1.69082428143753,15.071809088333));
#19611=CARTESIAN_POINT('Ctrl Pts',(-2.33137274895099,1.77334571203064,15.0683957111292));
#19612=CARTESIAN_POINT('Ctrl Pts',(-2.27155099682431,1.8530278346518,15.064982642569));
#19613=CARTESIAN_POINT('Ctrl Pts',(-2.23076137590659,1.90735930205439,15.0626554326866));
#19614=CARTESIAN_POINT('Ctrl Pts',(-2.18813878650124,1.96037022431859,15.0603283662998));
#19615=CARTESIAN_POINT('Ctrl Pts',(-2.14373220034752,2.0119373894844,15.058));
#19616=CARTESIAN_POINT('',(-2.,-2.44929359829471E-16,16.));
#19617=CARTESIAN_POINT('',(-2.5,-3.06161699786838E-16,15.5));
#19618=CARTESIAN_POINT('Origin',(0.,0.,16.));
#19619=CARTESIAN_POINT('Ctrl Pts',(1.70810875200393,-2.39535560853239,-0.329233991005387));
#19620=CARTESIAN_POINT('Ctrl Pts',(2.5000696979919,-1.83061464970825,-0.276613620635017));
#19621=CARTESIAN_POINT('Ctrl Pts',(3.46698259537958,0.135843711197753,-0.171372879894276));
#19622=CARTESIAN_POINT('Ctrl Pts',(1.78000461065578,2.98198357260362,-0.013511768783165));
#19623=CARTESIAN_POINT('Ctrl Pts',(-1.52068059202578,3.11864337292237,0.144349342327946));
#19624=CARTESIAN_POINT('Ctrl Pts',(-3.44323740053193,0.434868872546417,
0.302210453439058));
#19625=CARTESIAN_POINT('Ctrl Pts',(-2.24748662857037,-2.64500439253867,
0.460071564550167));
#19626=CARTESIAN_POINT('Ctrl Pts',(0.98413688813967,-3.32800743087112,0.61793267566128));
#19627=CARTESIAN_POINT('Ctrl Pts',(3.3242675736315,-0.997273536182889,0.775793786772391));
#19628=CARTESIAN_POINT('Ctrl Pts',(2.65350107828341,2.23705783115145,0.933654897883501));
#19629=CARTESIAN_POINT('Ctrl Pts',(-0.420704297245377,3.44500822120461,
1.09151600899461));
#19630=CARTESIAN_POINT('Ctrl Pts',(-3.11384086799285,1.53272940938773,1.24937712010572));
#19631=CARTESIAN_POINT('Ctrl Pts',(-2.98662452021757,-1.76786447124123,
1.40723823121684));
#19632=CARTESIAN_POINT('Ctrl Pts',(-0.154268773033873,-3.46719137695888,
1.56509934232795));
#19633=CARTESIAN_POINT('Ctrl Pts',(2.81781362814421,-2.02612228753563,1.72296045343906));
#19634=CARTESIAN_POINT('Ctrl Pts',(3.23766264061691,1.25011350527631,1.88082156455017));
#19635=CARTESIAN_POINT('Ctrl Pts',(0.724998218776244,3.39405562633926,2.03868267566128));
#19636=CARTESIAN_POINT('Ctrl Pts',(-2.44433298400306,2.46383378430329,2.19654378677239));
#19637=CARTESIAN_POINT('Ctrl Pts',(-3.39970985401105,-0.698006346200326,
2.35440489788351));
#19638=CARTESIAN_POINT('Ctrl Pts',(-1.27579956793912,-3.22762676650925,
2.51226600899461));
#19639=CARTESIAN_POINT('Ctrl Pts',(2.00366607964198,-2.83382462640088,2.67012712010573));
#19640=CARTESIAN_POINT('Ctrl Pts',(3.46831127903076,0.12671419166248,2.82798823121683));
#19641=CARTESIAN_POINT('Ctrl Pts',(1.79153366111842,2.9724815653929,2.98584934232795));
#19642=CARTESIAN_POINT('Ctrl Pts',(-1.50792549309295,3.12592391504671,3.14371045343906));
#19643=CARTESIAN_POINT('Ctrl Pts',(-3.44158119482194,0.448060782465637,
3.30157156455017));
#19644=CARTESIAN_POINT('Ctrl Pts',(-2.25802486298351,-2.63563337612261,
3.45943267566128));
#19645=CARTESIAN_POINT('Ctrl Pts',(0.970737398643871,-3.33210271331857,
3.61729378677239));
#19646=CARTESIAN_POINT('Ctrl Pts',(3.32025430017048,-1.01052014634333,3.7751548978835));
#19647=CARTESIAN_POINT('Ctrl Pts',(2.66245099976358,2.22634100195603,3.93301600899462));
#19648=CARTESIAN_POINT('Ctrl Pts',(-0.406867188726441,3.44669387613558,
4.09087712010572));
#19649=CARTESIAN_POINT('Ctrl Pts',(-3.10766543711734,1.54520390729755,4.24873823121684));
#19650=CARTESIAN_POINT('Ctrl Pts',(-2.99369583814259,-1.75585443953709,
4.40659934232795));
#19651=CARTESIAN_POINT('Ctrl Pts',(-0.16818635164463,-3.46654769699322,
4.56446045343906));
#19652=CARTESIAN_POINT('Ctrl Pts',(2.80965791624474,-2.03741551431062,4.72232156455017));
#19653=CARTESIAN_POINT('Ctrl Pts',(3.24265463709948,1.23710569022097,4.88018267566128));
#19654=CARTESIAN_POINT('Ctrl Pts',(0.738617048059715,3.39111846455234,5.0380437867724));
#19655=CARTESIAN_POINT('Ctrl Pts',(-2.43442290318405,2.47362582310745,5.1959048978835));
#19656=CARTESIAN_POINT('Ctrl Pts',(-3.40248440570545,-0.684353310232048,
5.35376600899462));
#19657=CARTESIAN_POINT('Ctrl Pts',(-1.28874579170717,-3.22247945977245,
5.51162712010572));
#19658=CARTESIAN_POINT('Ctrl Pts',(1.99227427239527,-2.84184496548404,5.66948823121683));
#19659=CARTESIAN_POINT('Ctrl Pts',(3.46879199270663,0.112790494414327,5.82734934232795));
#19660=CARTESIAN_POINT('Ctrl Pts',(1.803451502182,2.96526596843754,5.98521045343906));
#19661=CARTESIAN_POINT('Ctrl Pts',(-1.49536511544646,3.13195190828366,6.14307156455017));
#19662=CARTESIAN_POINT('Ctrl Pts',(-3.4397548386282,0.461872530499354,6.30093267566129));
#19663=CARTESIAN_POINT('Ctrl Pts',(-2.26858675213732,-2.62654787360198,
6.45879378677239));
#19664=CARTESIAN_POINT('Ctrl Pts',(0.957353695793138,-3.33597264458916,
6.61665489788351));
#19665=CARTESIAN_POINT('Ctrl Pts',(3.31617107144768,-1.02384032406894,6.77451600899461));
#19666=CARTESIAN_POINT('Ctrl Pts',(2.67136662968815,2.21563532967061,6.93237712010573));
#19667=CARTESIAN_POINT('Ctrl Pts',(-0.393028031746144,3.44829937078522,
7.09023823121684));
#19668=CARTESIAN_POINT('Ctrl Pts',(-3.10143756889894,1.55766639256237,7.24809934232795));
#19669=CARTESIAN_POINT('Ctrl Pts',(-3.00072015011765,-1.74382285940228,
7.40596045343905));
#19670=CARTESIAN_POINT('Ctrl Pts',(-0.182100573498421,-3.46584462511342,
7.56382156455018));
#19671=CARTESIAN_POINT('Ctrl Pts',(2.80145659039814,-2.04867775807003,7.72168267566128));
#19672=CARTESIAN_POINT('Ctrl Pts',(3.24759455782818,1.22407890769377,7.8795437867724));
#19673=CARTESIAN_POINT('Ctrl Pts',(0.752223882355328,3.38812615100299,8.03740489788349));
#19674=CARTESIAN_POINT('Ctrl Pts',(-2.42447354494764,2.4833782664236,8.19526600899462));
#19675=CARTESIAN_POINT('Ctrl Pts',(-3.40520415435994,-0.670689385204343,
8.35312712010572));
#19676=CARTESIAN_POINT('Ctrl Pts',(-1.30167123501543,-3.21728015258687,
8.51098823121684));
#19677=CARTESIAN_POINT('Ctrl Pts',(1.98085035420065,-2.84981954842042,8.66884934232795));
#19678=CARTESIAN_POINT('Ctrl Pts',(3.46921681308078,0.098864999537257,8.82671045343906));
#19679=CARTESIAN_POINT('Ctrl Pts',(1.81534028008778,2.95800257805621,8.98457156455017));
#19680=CARTESIAN_POINT('Ctrl Pts',(-1.4827806401293,3.13792943795007,9.14243267566127));
#19681=CARTESIAN_POINT('Ctrl Pts',(-3.4378730539225,0.475676832953572,9.3002937867724));
#19682=CARTESIAN_POINT('Ctrl Pts',(-2.27911208446667,-2.61742004476474,
9.45815489788349));
#19683=CARTESIAN_POINT('Ctrl Pts',(0.943954565772613,-3.3397888199782,9.61601600899462));
#19684=CARTESIAN_POINT('Ctrl Pts',(3.31203440522278,-1.03714400297725,9.77387712010572));
#19685=CARTESIAN_POINT('Ctrl Pts',(2.68023921253269,2.20489395389312,9.93173823121684));
#19686=CARTESIAN_POINT('Ctrl Pts',(-0.379182541400898,3.44984929882113,
10.0895993423279));
#19687=CARTESIAN_POINT('Ctrl Pts',(-3.09515972337558,1.57010377716378,10.2474604534391));
#19688=CARTESIAN_POINT('Ctrl Pts',(-3.00769610777576,-1.73176317886687,
10.4053215645502));
#19689=CARTESIAN_POINT('Ctrl Pts',(-0.196011860918037,-3.46508570377902,
10.5631826756613));
#19690=CARTESIAN_POINT('Ctrl Pts',(2.79321012116224,-2.05990698897259,10.7210437867724));
#19691=CARTESIAN_POINT('Ctrl Pts',(3.25248214612884,1.2110324001305,10.8789048978835));
#19692=CARTESIAN_POINT('Ctrl Pts',(0.765818594962506,3.38507924024569,11.0367660089946));
#19693=CARTESIAN_POINT('Ctrl Pts',(-2.41448511783304,2.49309069223908,11.1946271201057));
#19694=CARTESIAN_POINT('Ctrl Pts',(-3.40786903136843,-0.657014653010787,
11.3524882312168));
#19695=CARTESIAN_POINT('Ctrl Pts',(-1.3145757016765,-3.21202900045202,11.510349342328));
#19696=CARTESIAN_POINT('Ctrl Pts',(1.96939451380669,-2.85774821044889,11.668210453439));
#19697=CARTESIAN_POINT('Ctrl Pts',(3.46958573405997,0.0849379149034097,
11.8260715645502));
#19698=CARTESIAN_POINT('Ctrl Pts',(1.82719979676502,2.95069151525923,11.9839326756613));
#19699=CARTESIAN_POINT('Ctrl Pts',(-1.47017225488226,3.14385641459579,12.1417937867724));
#19700=CARTESIAN_POINT('Ctrl Pts',(-3.43593590116163,0.489473446687968,
12.2996548978835));
#19701=CARTESIAN_POINT('Ctrl Pts',(-2.28960063207268,-2.60824999320481,
12.4575160089946));
#19702=CARTESIAN_POINT('Ctrl Pts',(0.930540112760845,-3.34355126315401,
12.6153771201057));
#19703=CARTESIAN_POINT('Ctrl Pts',(3.30784458181684,-1.05043080491032,12.7732382312169));
#19704=CARTESIAN_POINT('Ctrl Pts',(2.68906819704165,2.19411673426304,12.9310993423279));
#19705=CARTESIAN_POINT('Ctrl Pts',(-0.365330160772045,3.45134423437463,
13.0889604534391));
#19706=CARTESIAN_POINT('Ctrl Pts',(-3.08883349189378,1.58251471600082,13.2468215645502));
#19707=CARTESIAN_POINT('Ctrl Pts',(-3.01462075186278,-1.71967340539697,
13.4046826756613));
#19708=CARTESIAN_POINT('Ctrl Pts',(-0.209925428309919,-3.46427512302224,
13.5625437867724));
#19709=CARTESIAN_POINT('Ctrl Pts',(2.78492903121011,-2.07109504482717,13.7204048978835));
#19710=CARTESIAN_POINT('Ctrl Pts',(3.25729747472216,1.19795113049603,13.8782660089946));
#19711=CARTESIAN_POINT('Ctrl Pts',(0.779438885227093,3.38200690959721,14.0361271201057));
#19712=CARTESIAN_POINT('Ctrl Pts',(-2.40453022224261,2.50270729758603,14.1939882312168));
#19713=CARTESIAN_POINT('Ctrl Pts',(-3.41034060095634,-0.643223025084935,
14.351849342328));
#19714=CARTESIAN_POINT('Ctrl Pts',(-1.3277234162215,-3.20692920286191,14.5097104534391));
#19715=CARTESIAN_POINT('Ctrl Pts',(1.95841253548915,-2.86524258546647,14.6675715645502));
#19716=CARTESIAN_POINT('Ctrl Pts',(3.46892903525912,0.0702659147297645,
14.8254326756613));
#19717=CARTESIAN_POINT('Ctrl Pts',(1.8409162673649,2.94476989555806,14.9832937867724));
#19718=CARTESIAN_POINT('Ctrl Pts',(-1.46144261101867,3.14684084841223,15.1411548978835));
#19719=CARTESIAN_POINT('Ctrl Pts',(-2.76985851330384,1.3890220685151,15.2463956386242));
#19720=CARTESIAN_POINT('Ctrl Pts',(-2.91090525077878,0.426608275808748,
15.2990160089946));
#19721=CARTESIAN_POINT('Ctrl Pts',(1.59774743137963,-2.24059110187414,-0.219489327336926));
#19722=CARTESIAN_POINT('Ctrl Pts',(2.33853958862414,-1.71233819332979,-0.166868956966556));
#19723=CARTESIAN_POINT('Ctrl Pts',(3.24298000926863,0.127066816079881,-0.061628216225815));
#19724=CARTESIAN_POINT('Ctrl Pts',(1.66499808117169,2.78931689094975,0.0962328948852963));
#19725=CARTESIAN_POINT('Ctrl Pts',(-1.42242905026252,2.9171470684346,0.254094005996407));
#19726=CARTESIAN_POINT('Ctrl Pts',(-3.22076899721748,0.406771889250497,
0.411955117107519));
#19727=CARTESIAN_POINT('Ctrl Pts',(-2.10227597256058,-2.4741100174146,0.56981622821863));
#19728=CARTESIAN_POINT('Ctrl Pts',(0.9205515651778,-3.11298406383574,0.72767733932974));
#19729=CARTESIAN_POINT('Ctrl Pts',(3.10948583967916,-0.932839451205724,
0.885538450440853));
#19730=CARTESIAN_POINT('Ctrl Pts',(2.48205773023319,2.09252098227156,1.04339956155196));
#19731=CARTESIAN_POINT('Ctrl Pts',(-0.393522490594119,3.22242540473713,
1.20126067266308));
#19732=CARTESIAN_POINT('Ctrl Pts',(-2.91265485451303,1.43369939061326,1.35912178377418));
#19733=CARTESIAN_POINT('Ctrl Pts',(-2.79365798581306,-1.65364231910831,
1.5169828948853));
#19734=CARTESIAN_POINT('Ctrl Pts',(-0.144301430203291,-3.24317530141947,
1.67484400599641));
#19735=CARTESIAN_POINT('Ctrl Pts',(2.6357540064074,-1.8952140352733,1.83270511710752));
#19736=CARTESIAN_POINT('Ctrl Pts',(3.02847647238534,1.16934336859111,1.99056622821863));
#19737=CARTESIAN_POINT('Ctrl Pts',(0.67815590807408,3.17476486938028,2.14842733932974));
#19738=CARTESIAN_POINT('Ctrl Pts',(-2.28640403724036,2.30464488610489,2.30628845044085));
#19739=CARTESIAN_POINT('Ctrl Pts',(-3.18005377603123,-0.652907986929923,
2.46414956155196));
#19740=CARTESIAN_POINT('Ctrl Pts',(-1.19336984851725,-3.01908901853714,
2.62201067266307));
#19741=CARTESIAN_POINT('Ctrl Pts',(1.87420872841654,-2.65073053018457,2.77987178377419));
#19742=CARTESIAN_POINT('Ctrl Pts',(3.24422284634695,0.118527157015377,2.9377328948853));
#19743=CARTESIAN_POINT('Ctrl Pts',(1.67578223688854,2.78042881072881,3.09559400599641));
#19744=CARTESIAN_POINT('Ctrl Pts',(-1.41049806136441,2.92395721296701,3.25345511710752));
#19745=CARTESIAN_POINT('Ctrl Pts',(-3.21921979935999,0.419111466671254,
3.41131622821863));
#19746=CARTESIAN_POINT('Ctrl Pts',(-2.11213332909314,-2.46534446464132,
3.56917733932974));
#19747=CARTESIAN_POINT('Ctrl Pts',(0.908017819947236,-3.11681474909129,
3.72703845044085));
#19748=CARTESIAN_POINT('Ctrl Pts',(3.10573186478955,-0.94523019467185,3.88489956155197));
#19749=CARTESIAN_POINT('Ctrl Pts',(2.49042939511648,2.08249657000891,4.04276067266307));
#19750=CARTESIAN_POINT('Ctrl Pts',(-0.380579401011611,3.2240021490943,4.20062178377419));
#19751=CARTESIAN_POINT('Ctrl Pts',(-2.90687841972373,1.44536790818848,4.3584828948853));
#19752=CARTESIAN_POINT('Ctrl Pts',(-2.8002724241724,-1.64240825846459,4.5163440059964));
#19753=CARTESIAN_POINT('Ctrl Pts',(-0.157319790685473,-3.24257320977247,
4.67420511710753));
#19754=CARTESIAN_POINT('Ctrl Pts',(2.62812523703122,-1.90577760392813,4.83206622821863));
#19755=CARTESIAN_POINT('Ctrl Pts',(3.03314593476479,1.15717599162043,4.98992733932975));
#19756=CARTESIAN_POINT('Ctrl Pts',(0.690894821495446,3.17201747832858,5.14778845044085));
#19757=CARTESIAN_POINT('Ctrl Pts',(-2.27713424914591,2.31380425890769,5.30564956155197));
#19758=CARTESIAN_POINT('Ctrl Pts',(-3.18264906326793,-0.640137076925948,
5.46351067266308));
#19759=CARTESIAN_POINT('Ctrl Pts',(-1.20547961362863,-3.01427428053665,
5.62137178377419));
#19760=CARTESIAN_POINT('Ctrl Pts',(1.86355294859817,-2.65823267321491,5.7792328948853));
#19761=CARTESIAN_POINT('Ctrl Pts',(3.24467250099567,0.105503073222438,5.93709400599641));
#19762=CARTESIAN_POINT('Ctrl Pts',(1.68693006335134,2.77367941524228,6.09495511710752));
#19763=CARTESIAN_POINT('Ctrl Pts',(-1.39874921276312,2.92959573609933,6.25281622821863));
#19764=CARTESIAN_POINT('Ctrl Pts',(-3.21751144448276,0.432030834315646,
6.41067733932974));
#19765=CARTESIAN_POINT('Ctrl Pts',(-2.12201281202782,-2.45684597864148,
6.56853845044085));
#19766=CARTESIAN_POINT('Ctrl Pts',(0.895498841382776,-3.12043464316416,
6.72639956155197));
#19767=CARTESIAN_POINT('Ctrl Pts',(3.10191245446456,-0.957689752484927,
6.88426067266308));
#19768=CARTESIAN_POINT('Ctrl Pts',(2.4987689840299,2.07248259380561,7.04212178377418));
#19769=CARTESIAN_POINT('Ctrl Pts',(-0.367634395319329,3.22550391234535,
7.1999828948853));
#19770=CARTESIAN_POINT('Ctrl Pts',(-2.90105293558095,1.45702518925863,7.3578440059964));
#19771=CARTESIAN_POINT('Ctrl Pts',(-2.8068428936476,-1.63115404163953,7.51570511710752));
#19772=CARTESIAN_POINT('Ctrl Pts',(-0.170335011291572,-3.24191556353729,
7.67356622821863));
#19773=CARTESIAN_POINT('Ctrl Pts',(2.62045380083611,-1.91631219138755,7.83142733932975));
#19774=CARTESIAN_POINT('Ctrl Pts',(3.03776668601744,1.14499087267086,7.98928845044085));
#19775=CARTESIAN_POINT('Ctrl Pts',(0.703622514928034,3.16921849888318,8.14714956155197));
#19776=CARTESIAN_POINT('Ctrl Pts',(-2.26782772135753,2.32292659449655,8.30501067266308));
#19777=CARTESIAN_POINT('Ctrl Pts',(-3.18519308830241,-0.627355981407313,
8.46287178377418));
#19778=CARTESIAN_POINT('Ctrl Pts',(-1.21756994091078,-3.00941090184898,
8.62073289488531));
#19779=CARTESIAN_POINT('Ctrl Pts',(1.852867132528,-2.6656920164142,8.77859400599641));
#19780=CARTESIAN_POINT('Ctrl Pts',(3.24506987362244,0.0924773079458306,
8.93645511710752));
#19781=CARTESIAN_POINT('Ctrl Pts',(1.698050704434,2.7668853142746,9.09431622821864));
#19782=CARTESIAN_POINT('Ctrl Pts',(-1.3869778234475,2.93518705612466,9.25217733932973));
#19783=CARTESIAN_POINT('Ctrl Pts',(-3.21575124234316,0.444943237441223,
9.41003845044086));
#19784=CARTESIAN_POINT('Ctrl Pts',(-2.13185810008334,-2.44830790103859,
9.56789956155196));
#19785=CARTESIAN_POINT('Ctrl Pts',(0.882965432401702,-3.12400425453603,
9.72576067266308));
#19786=CARTESIAN_POINT('Ctrl Pts',(3.09804305924746,-0.970133877473286,
9.88362178377418));
#19787=CARTESIAN_POINT('Ctrl Pts',(2.50706830714555,2.06243522092151,10.0414828948853));
#19788=CARTESIAN_POINT('Ctrl Pts',(-0.354683465462343,3.22695369915506,
10.1993440059964));
#19789=CARTESIAN_POINT('Ctrl Pts',(-2.89518070317902,1.4686589914253,10.3572051171075));
#19790=CARTESIAN_POINT('Ctrl Pts',(-2.81336813298999,-1.61987353998757,
10.5150662282186));
#19791=CARTESIAN_POINT('Ctrl Pts',(-0.183347487058001,-3.24120567629433,
10.6729273393297));
#19792=CARTESIAN_POINT('Ctrl Pts',(2.61274013797703,-1.9268158989588,10.8307884504409));
#19793=CARTESIAN_POINT('Ctrl Pts',(3.04233848605292,1.13278730312457,10.988649561552));
#19794=CARTESIAN_POINT('Ctrl Pts',(0.716338869857416,3.16636844976869,11.1465106726631));
#19795=CARTESIAN_POINT('Ctrl Pts',(-2.25848464894066,2.33201149812516,11.3043717837742));
#19796=CARTESIAN_POINT('Ctrl Pts',(-3.18768578696123,-0.61456477697643,
11.4622328948853));
#19797=CARTESIAN_POINT('Ctrl Pts',(-1.22964064685199,-3.00449902792679,
11.6200940059964));
#19798=CARTESIAN_POINT('Ctrl Pts',(1.84215145675955,-2.67310840566659,11.7779551171075));
#19799=CARTESIAN_POINT('Ctrl Pts',(3.24541495852771,0.0794500556270124,
11.9358162282186));
#19800=CARTESIAN_POINT('Ctrl Pts',(1.70914397486321,2.76004662101762,12.0936773393297));
#19801=CARTESIAN_POINT('Ctrl Pts',(-1.37518406902836,2.94073108937221,12.2515384504409));
#19802=CARTESIAN_POINT('Ctrl Pts',(-3.21393924949186,0.457848448617044,
12.409399561552));
#19803=CARTESIAN_POINT('Ctrl Pts',(-2.14166898008542,-2.43973032873338,
12.5672606726631));
#19804=CARTESIAN_POINT('Ctrl Pts',(0.870417690451563,-3.12752360534598,
12.7251217837742));
#19805=CARTESIAN_POINT('Ctrl Pts',(3.09412394134766,-0.98256221591188,12.8829828948853));
#19806=CARTESIAN_POINT('Ctrl Pts',(2.51532684882466,2.05235432006483,13.0408440059964));
#19807=CARTESIAN_POINT('Ctrl Pts',(-0.341726090504644,3.22835204655998,
13.1987051171075));
#19808=CARTESIAN_POINT('Ctrl Pts',(-2.88926321104715,1.48026805649486,13.3565662282186));
#19809=CARTESIAN_POINT('Ctrl Pts',(-2.81984537414356,-1.60856488971291,
13.5144273393297));
#19810=CARTESIAN_POINT('Ctrl Pts',(-0.196362095487134,-3.24044746735677,
13.6722884504409));
#19811=CARTESIAN_POINT('Ctrl Pts',(2.60499409125458,-1.93728109181189,13.830149561552));
#19812=CARTESIAN_POINT('Ctrl Pts',(3.04684269509828,1.12055121749295,13.9880106726631));
#19813=CARTESIAN_POINT('Ctrl Pts',(0.729079149865556,3.16349462314833,14.1458717837742));
#19814=CARTESIAN_POINT('Ctrl Pts',(-2.24917294156805,2.34100677226896,14.3037328948853));
#19815=CARTESIAN_POINT('Ctrl Pts',(-3.1899976678388,-0.601664229474863,
14.4615940059964));
#19816=CARTESIAN_POINT('Ctrl Pts',(-1.24193888437236,-2.9997287294955,14.6194551171075));
#19817=CARTESIAN_POINT('Ctrl Pts',(1.83187902672385,-2.68011856729716,14.7773162282186));
#19818=CARTESIAN_POINT('Ctrl Pts',(3.24480068919561,0.0657260169420378,
14.9351773393297));
#19819=CARTESIAN_POINT('Ctrl Pts',(1.72197422097186,2.75450759860113,15.0930384504409));
#19820=CARTESIAN_POINT('Ctrl Pts',(-1.36701844957144,2.94352269819615,15.250899561552));
#19821=CARTESIAN_POINT('Ctrl Pts',(-2.59089728316432,1.29927701587847,15.3561403022927));
#19822=CARTESIAN_POINT('Ctrl Pts',(-2.72283095673204,0.399045011670964,
15.4087606726631));
#19823=CARTESIAN_POINT('Ctrl Pts',(1.48738611075532,-2.0858265952159,-0.109744663668465));
#19824=CARTESIAN_POINT('Ctrl Pts',(2.17700947925639,-1.59406173695134,-0.0571242932980945));
#19825=CARTESIAN_POINT('Ctrl Pts',(3.01897742315769,0.118289920962009,0.0481164474426461));
#19826=CARTESIAN_POINT('Ctrl Pts',(1.5499915516876,2.59665020929587,0.205977558553758));
#19827=CARTESIAN_POINT('Ctrl Pts',(-1.32417750849926,2.71565076394683,0.363838669664868));
#19828=CARTESIAN_POINT('Ctrl Pts',(-2.99830059390304,0.37867490595458,0.521699780775981));
#19829=CARTESIAN_POINT('Ctrl Pts',(-1.95706531655079,-2.30321564229053,
0.679560891887089));
#19830=CARTESIAN_POINT('Ctrl Pts',(0.856966242215927,-2.89796069680035,
0.837422002998203));
#19831=CARTESIAN_POINT('Ctrl Pts',(2.89470410572683,-0.86840536622856,0.995283114109312));
#19832=CARTESIAN_POINT('Ctrl Pts',(2.31061438218297,1.94798413339166,1.15314422522042));
#19833=CARTESIAN_POINT('Ctrl Pts',(-0.36634068394286,2.99984258826965,1.31100533633153));
#19834=CARTESIAN_POINT('Ctrl Pts',(-2.71146884103322,1.33466937183879,1.46886644744265));
#19835=CARTESIAN_POINT('Ctrl Pts',(-2.60069145140856,-1.53942016697539,
1.62672755855376));
#19836=CARTESIAN_POINT('Ctrl Pts',(-0.134334087372704,-3.01915922588007,
1.78458866966487));
#19837=CARTESIAN_POINT('Ctrl Pts',(2.45369438467058,-1.76430578301097,1.94244978077598));
#19838=CARTESIAN_POINT('Ctrl Pts',(2.81929030415377,1.0885732319059,2.10031089188709));
#19839=CARTESIAN_POINT('Ctrl Pts',(0.63131359737191,2.95547411242131,2.2581720029982));
#19840=CARTESIAN_POINT('Ctrl Pts',(-2.12847509047765,2.14545598790649,2.41603311410931));
#19841=CARTESIAN_POINT('Ctrl Pts',(-2.96039769805142,-0.607809627659522,
2.57389422522043));
#19842=CARTESIAN_POINT('Ctrl Pts',(-1.11094012909538,-2.81055127056503,
2.73175533633153));
#19843=CARTESIAN_POINT('Ctrl Pts',(1.74475137719111,-2.46763643396825,2.88961644744264));
#19844=CARTESIAN_POINT('Ctrl Pts',(3.02013441366314,0.110340122368272,3.04747755855376));
#19845=CARTESIAN_POINT('Ctrl Pts',(1.56003081265866,2.58837605606472,3.20533866966487));
#19846=CARTESIAN_POINT('Ctrl Pts',(-1.31307062963587,2.72199051088731,3.36319978077598));
#19847=CARTESIAN_POINT('Ctrl Pts',(-2.99685840389804,0.390162150876873,
3.52106089188709));
#19848=CARTESIAN_POINT('Ctrl Pts',(-1.96624179520275,-2.29505555316004,
3.6789220029982));
#19849=CARTESIAN_POINT('Ctrl Pts',(0.845298241250599,-2.90152678486402,
3.83678311410932));
#19850=CARTESIAN_POINT('Ctrl Pts',(2.89120942940861,-0.879940243000373,
3.99464422522043));
#19851=CARTESIAN_POINT('Ctrl Pts',(2.31840779046938,1.93865213806179,4.15250533633154));
#19852=CARTESIAN_POINT('Ctrl Pts',(-0.354291613296782,3.00131042205302,
4.31036644744265));
#19853=CARTESIAN_POINT('Ctrl Pts',(-2.70609140233011,1.34553190907942,4.46822755855376));
#19854=CARTESIAN_POINT('Ctrl Pts',(-2.60684901020221,-1.52896207739209,
4.62608866966487));
#19855=CARTESIAN_POINT('Ctrl Pts',(-0.146453229726317,-3.01859872255171,
4.78394978077598));
#19856=CARTESIAN_POINT('Ctrl Pts',(2.44659255781772,-1.77413969354566,4.94181089188709));
#19857=CARTESIAN_POINT('Ctrl Pts',(2.82363723243009,1.07724629301989,5.09967200299821));
#19858=CARTESIAN_POINT('Ctrl Pts',(0.643172594931182,2.95291649210482,5.25753311410931));
#19859=CARTESIAN_POINT('Ctrl Pts',(-2.11984559510778,2.15398269470792,5.41539422522043));
#19860=CARTESIAN_POINT('Ctrl Pts',(-2.96281372083041,-0.595920843619846,
5.57325533633153));
#19861=CARTESIAN_POINT('Ctrl Pts',(-1.12221343555009,-2.80606910130085,
5.73111644744265));
#19862=CARTESIAN_POINT('Ctrl Pts',(1.73483162480106,-2.47462038094578,5.88897755855376));
#19863=CARTESIAN_POINT('Ctrl Pts',(3.02055300928471,0.0982156520305535,
6.04683866966487));
#19864=CARTESIAN_POINT('Ctrl Pts',(1.57040862452068,2.58209286204701,6.20469978077598));
#19865=CARTESIAN_POINT('Ctrl Pts',(-1.30213331007977,2.72723956391501,6.36256089188709));
#19866=CARTESIAN_POINT('Ctrl Pts',(-2.99526805033731,0.402189138131933,
6.52042200299821));
#19867=CARTESIAN_POINT('Ctrl Pts',(-1.97543887191833,-2.28714408368097,
6.67828311410931));
#19868=CARTESIAN_POINT('Ctrl Pts',(0.833643986972413,-2.90489664173917,
6.83614422522043));
#19869=CARTESIAN_POINT('Ctrl Pts',(2.88765383748144,-0.891539180900916,
6.99400533633154));
#19870=CARTESIAN_POINT('Ctrl Pts',(2.32617133837164,1.9293298579406,7.15186644744265));
#19871=CARTESIAN_POINT('Ctrl Pts',(-0.342240758892514,3.00270845390548,
7.30972755855377));
#19872=CARTESIAN_POINT('Ctrl Pts',(-2.70066830226297,1.35638398595488,7.46758866966487));
#19873=CARTESIAN_POINT('Ctrl Pts',(-2.61296563717754,-1.51848522387679,
7.62544978077598));
#19874=CARTESIAN_POINT('Ctrl Pts',(-0.158569449084724,-3.01798650196116,
7.78331089188708));
#19875=CARTESIAN_POINT('Ctrl Pts',(2.43945101127409,-1.78394662470507,7.94117200299821));
#19876=CARTESIAN_POINT('Ctrl Pts',(2.8279388142067,1.06590283764795,8.09903311410931));
#19877=CARTESIAN_POINT('Ctrl Pts',(0.655021147500741,2.95031084676337,8.25689422522044));
#19878=CARTESIAN_POINT('Ctrl Pts',(-2.11118189776743,2.16247492256949,8.41475533633153));
#19879=CARTESIAN_POINT('Ctrl Pts',(-2.96518202224487,-0.584022577610279,
8.57261644744266));
#19880=CARTESIAN_POINT('Ctrl Pts',(-1.13346864680612,-2.8015416511111,8.73047755855375));
#19881=CARTESIAN_POINT('Ctrl Pts',(1.72488391085535,-2.48156448440799,8.88833866966489));
#19882=CARTESIAN_POINT('Ctrl Pts',(3.0209229341641,0.0860896163543999,9.04619978077597));
#19883=CARTESIAN_POINT('Ctrl Pts',(1.58076112878023,2.575768050493,9.2040608918871));
#19884=CARTESIAN_POINT('Ctrl Pts',(-1.2911750067657,2.73244467429924,9.3619220029982));
#19885=CARTESIAN_POINT('Ctrl Pts',(-2.99362943076381,0.414209641928883,
9.51978311410932));
#19886=CARTESIAN_POINT('Ctrl Pts',(-1.98460411570002,-2.27919575731244,
9.67764422522042));
#19887=CARTESIAN_POINT('Ctrl Pts',(0.821976299030791,-2.90821968909385,
9.83550533633154));
#19888=CARTESIAN_POINT('Ctrl Pts',(2.88405171327213,-0.903123751969326,
9.99336644744264));
#19889=CARTESIAN_POINT('Ctrl Pts',(2.33389740175841,1.9199764879499,10.1512275585538));
#19890=CARTESIAN_POINT('Ctrl Pts',(-0.330184389523787,3.00405809948898,
10.3090886696649));
#19891=CARTESIAN_POINT('Ctrl Pts',(-2.69520168298246,1.36721420568682,10.466949780776));
#19892=CARTESIAN_POINT('Ctrl Pts',(-2.61904015820422,-1.50798390110827,
10.6248108918871));
#19893=CARTESIAN_POINT('Ctrl Pts',(-0.170683113197963,-3.01732564880962,
10.7826720029982));
#19894=CARTESIAN_POINT('Ctrl Pts',(2.43227015479182,-1.793724808945,10.9405331141093));
#19895=CARTESIAN_POINT('Ctrl Pts',(2.83219482597701,1.05454220611865,11.0983942252204));
#19896=CARTESIAN_POINT('Ctrl Pts',(0.666859144752323,2.94765765929168,11.2562553363315));
#19897=CARTESIAN_POINT('Ctrl Pts',(-2.10248418004828,2.17093230401124,11.4141164474427));
#19898=CARTESIAN_POINT('Ctrl Pts',(-2.96750254255404,-0.572114900942073,
11.5719775585538));
#19899=CARTESIAN_POINT('Ctrl Pts',(-1.14470559202747,-2.79696905540156,
11.7298386696649));
#19900=CARTESIAN_POINT('Ctrl Pts',(1.7149083997124,-2.48846860088429,11.887699780776));
#19901=CARTESIAN_POINT('Ctrl Pts',(3.02124418299545,0.0739621963506113,
12.0455608918871));
#19902=CARTESIAN_POINT('Ctrl Pts',(1.5910881529614,2.56940172677601,12.2034220029982));
#19903=CARTESIAN_POINT('Ctrl Pts',(-1.28019588317448,2.73760576414863,12.3612831141093));
#19904=CARTESIAN_POINT('Ctrl Pts',(-2.99194259782208,0.42622345054612,12.5191442252204));
#19905=CARTESIAN_POINT('Ctrl Pts',(-1.99373732809816,-2.27121066426194,
12.6770053363315));
#19906=CARTESIAN_POINT('Ctrl Pts',(0.810295268142284,-2.91149594753796,
12.8348664474426));
#19907=CARTESIAN_POINT('Ctrl Pts',(2.88040330087848,-0.914693626913434,
12.9927275585538));
#19908=CARTESIAN_POINT('Ctrl Pts',(2.34158550060768,1.91059190586663,13.1505886696649));
#19909=CARTESIAN_POINT('Ctrl Pts',(-0.318122020237242,3.00535985874532,
13.308449780776));
#19910=CARTESIAN_POINT('Ctrl Pts',(-2.68969293020052,1.37802139698889,13.4663108918871));
#19911=CARTESIAN_POINT('Ctrl Pts',(-2.62506999642434,-1.49745637402886,
13.6241720029982));
#19912=CARTESIAN_POINT('Ctrl Pts',(-0.182798762664348,-3.0166198116913,
13.7820331141093));
#19913=CARTESIAN_POINT('Ctrl Pts',(2.42505915129906,-1.80346713879661,13.9398942252204));
#19914=CARTESIAN_POINT('Ctrl Pts',(2.8363879154744,1.04315130448987,14.0977553363316));
#19915=CARTESIAN_POINT('Ctrl Pts',(0.678719414504022,2.94498233669946,14.2556164474426));
#19916=CARTESIAN_POINT('Ctrl Pts',(-2.09381566089348,2.17930624695187,14.4134775585538));
#19917=CARTESIAN_POINT('Ctrl Pts',(-2.96965473472126,-0.560105433864789,
14.5713386696649));
#19918=CARTESIAN_POINT('Ctrl Pts',(-1.15615435252323,-2.79252825612909,
14.729199780776));
#19919=CARTESIAN_POINT('Ctrl Pts',(1.70534551795855,-2.49499454912784,14.8870608918871));
#19920=CARTESIAN_POINT('Ctrl Pts',(3.0206723431321,0.0611861191543108,15.0449220029982));
#19921=CARTESIAN_POINT('Ctrl Pts',(1.60303217457882,2.56424530164419,15.2027831141093));
#19922=CARTESIAN_POINT('Ctrl Pts',(-1.27259428812422,2.74020454798006,15.3606442252204));
#19923=CARTESIAN_POINT('Ctrl Pts',(-2.41193605302479,1.20953196324185,15.4658849659612));
#19924=CARTESIAN_POINT('Ctrl Pts',(-2.53475666268529,0.371481747533179,
15.5185053363315));
#19925=CARTESIAN_POINT('Ctrl Pts',(1.37702479013102,-1.93106208855765,-3.60822483003176E-15));
#19926=CARTESIAN_POINT('Ctrl Pts',(2.01547936988864,-1.47578528057288,0.0526203703703667));
#19927=CARTESIAN_POINT('Ctrl Pts',(2.79497483704674,0.109513025844136,0.157861111111108));
#19928=CARTESIAN_POINT('Ctrl Pts',(1.4349850222035,2.40398352764199,0.315722222222219));
#19929=CARTESIAN_POINT('Ctrl Pts',(-1.225925966736,2.51415445945906,0.473583333333329));
#19930=CARTESIAN_POINT('Ctrl Pts',(-2.77583219058859,0.350577922658662,
0.631444444444441));
#19931=CARTESIAN_POINT('Ctrl Pts',(-1.811854660541,-2.13232126716645,0.789305555555552));
#19932=CARTESIAN_POINT('Ctrl Pts',(0.793380919254056,-2.68293732976497,
0.947166666666663));
#19933=CARTESIAN_POINT('Ctrl Pts',(2.67992237177449,-0.803971281251394,
1.10502777777777));
#19934=CARTESIAN_POINT('Ctrl Pts',(2.13917103413275,1.80344728451176,1.26288888888888));
#19935=CARTESIAN_POINT('Ctrl Pts',(-0.339158877291603,2.77725977180218,
1.42075));
#19936=CARTESIAN_POINT('Ctrl Pts',(-2.51028282755341,1.23563935306431,1.57861111111111));
#19937=CARTESIAN_POINT('Ctrl Pts',(-2.40772491700405,-1.42519801484247,
1.73647222222222));
#19938=CARTESIAN_POINT('Ctrl Pts',(-0.124366744542119,-2.79514315034066,
1.89433333333333));
#19939=CARTESIAN_POINT('Ctrl Pts',(2.27163476293377,-1.63339753074864,2.05219444444444));
#19940=CARTESIAN_POINT('Ctrl Pts',(2.61010413592219,1.00780309522069,2.21005555555555));
#19941=CARTESIAN_POINT('Ctrl Pts',(0.584471286669745,2.73618335546233,2.36791666666667));
#19942=CARTESIAN_POINT('Ctrl Pts',(-1.97054614371495,1.98626708970809,2.52577777777777));
#19943=CARTESIAN_POINT('Ctrl Pts',(-2.7407416200716,-0.562711268389121,
2.68363888888889));
#19944=CARTESIAN_POINT('Ctrl Pts',(-1.02851040967351,-2.60201352259292,
2.84149999999999));
#19945=CARTESIAN_POINT('Ctrl Pts',(1.61529402596567,-2.28454233775194,2.99936111111111));
#19946=CARTESIAN_POINT('Ctrl Pts',(2.79604598097933,0.102153087721166,3.15722222222222));
#19947=CARTESIAN_POINT('Ctrl Pts',(1.44427938842878,2.39632330140064,3.31508333333333));
#19948=CARTESIAN_POINT('Ctrl Pts',(-1.21564319790733,2.5200238088076,3.47294444444445));
#19949=CARTESIAN_POINT('Ctrl Pts',(-2.77449700843608,0.361212835082494,
3.63080555555555));
#19950=CARTESIAN_POINT('Ctrl Pts',(-1.82035026131238,-2.12476664167876,
3.78866666666667));
#19951=CARTESIAN_POINT('Ctrl Pts',(0.782578662553965,-2.68623882063674,
3.94652777777777));
#19952=CARTESIAN_POINT('Ctrl Pts',(2.67668699402767,-0.814650291328897,
4.10438888888889));
#19953=CARTESIAN_POINT('Ctrl Pts',(2.14638618582228,1.79480770611467,4.26225));
#19954=CARTESIAN_POINT('Ctrl Pts',(-0.328003825581952,2.77861869501174,
4.42011111111111));
#19955=CARTESIAN_POINT('Ctrl Pts',(-2.50530438493649,1.24569590997036,4.57797222222222));
#19956=CARTESIAN_POINT('Ctrl Pts',(-2.41342559623202,-1.41551589631959,
4.73583333333333));
#19957=CARTESIAN_POINT('Ctrl Pts',(-0.135586668767159,-2.79462423533096,
4.89369444444444));
#19958=CARTESIAN_POINT('Ctrl Pts',(2.2650598786042,-1.64250178316317,5.05155555555556));
#19959=CARTESIAN_POINT('Ctrl Pts',(2.61412853009539,0.997316594419356,5.20941666666666));
#19960=CARTESIAN_POINT('Ctrl Pts',(0.595450368366912,2.73381550588105,5.36727777777778));
#19961=CARTESIAN_POINT('Ctrl Pts',(-1.96255694106964,1.99416113050815,5.52513888888888));
#19962=CARTESIAN_POINT('Ctrl Pts',(-2.74297837839289,-0.551704610313744,
5.683));
#19963=CARTESIAN_POINT('Ctrl Pts',(-1.03894725747156,-2.59786392206505,
5.84086111111111));
#19964=CARTESIAN_POINT('Ctrl Pts',(1.60611030100396,-2.29100808867664,5.99872222222222));
#19965=CARTESIAN_POINT('Ctrl Pts',(2.79643351757374,0.090928230838667,6.15658333333333));
#19966=CARTESIAN_POINT('Ctrl Pts',(1.45388718569001,2.39050630885174,6.31444444444444));
#19967=CARTESIAN_POINT('Ctrl Pts',(-1.20551740739643,2.52488339173069,6.47230555555556));
#19968=CARTESIAN_POINT('Ctrl Pts',(-2.77302465619186,0.372347441948222,
6.63016666666666));
#19969=CARTESIAN_POINT('Ctrl Pts',(-1.82886493180883,-2.11744218872047,
6.78802777777778));
#19970=CARTESIAN_POINT('Ctrl Pts',(0.771789132562049,-2.68935864031417,
6.94588888888888));
#19971=CARTESIAN_POINT('Ctrl Pts',(2.67339522049833,-0.825388609316905,
7.10375));
#19972=CARTESIAN_POINT('Ctrl Pts',(2.15357369271338,1.7861771220756,7.26161111111111));
#19973=CARTESIAN_POINT('Ctrl Pts',(-0.3168471224657,2.77991299546561,7.41947222222222));
#19974=CARTESIAN_POINT('Ctrl Pts',(-2.50028366894498,1.25574278265114,7.57733333333334));
#19975=CARTESIAN_POINT('Ctrl Pts',(-2.41908838070749,-1.40581640611404,
7.73519444444443));
#19976=CARTESIAN_POINT('Ctrl Pts',(-0.146803886877873,-2.79405744038503,
7.89305555555557));
#19977=CARTESIAN_POINT('Ctrl Pts',(2.25844822171206,-1.65158105802259,8.05091666666665));
#19978=CARTESIAN_POINT('Ctrl Pts',(2.61811094239596,0.986814802625037,8.20877777777778));
#19979=CARTESIAN_POINT('Ctrl Pts',(0.606419780073446,2.73140319464357,8.36663888888888));
#19980=CARTESIAN_POINT('Ctrl Pts',(-1.95453607417732,2.00202325064244,8.52450000000001));
#19981=CARTESIAN_POINT('Ctrl Pts',(-2.74517095618734,-0.540689173813247,
8.68236111111111));
#19982=CARTESIAN_POINT('Ctrl Pts',(-1.04936735270146,-2.59367240037321,
8.84022222222223));
#19983=CARTESIAN_POINT('Ctrl Pts',(1.59690068918271,-2.29743695240177,8.99808333333332));
#19984=CARTESIAN_POINT('Ctrl Pts',(2.79677599470576,0.0797019247629725,
9.15594444444445));
#19985=CARTESIAN_POINT('Ctrl Pts',(1.46347155312646,2.38465078671139,9.31380555555555));
#19986=CARTESIAN_POINT('Ctrl Pts',(-1.19537219008389,2.52970229247383,9.47166666666666));
#19987=CARTESIAN_POINT('Ctrl Pts',(-2.77150761918447,0.383476046416537,
9.62952777777778));
#19988=CARTESIAN_POINT('Ctrl Pts',(-1.83735013131669,-2.1100836135863,9.78738888888888));
#19989=CARTESIAN_POINT('Ctrl Pts',(0.760987165659879,-2.69243512365168,
9.94525));
#19990=CARTESIAN_POINT('Ctrl Pts',(2.6700603672968,-0.836113626465368,10.1031111111111));
#19991=CARTESIAN_POINT('Ctrl Pts',(2.16072649637127,1.7775177549783,10.2609722222222));
#19992=CARTESIAN_POINT('Ctrl Pts',(-0.305685313585232,2.78116249982291,
10.4188333333333));
#19993=CARTESIAN_POINT('Ctrl Pts',(-2.4952226627859,1.26576941994835,10.5766944444444));
#19994=CARTESIAN_POINT('Ctrl Pts',(-2.42471218341845,-1.39609426222898,
10.7345555555556));
#19995=CARTESIAN_POINT('Ctrl Pts',(-0.158018739337926,-2.79344562132492,
10.8924166666667));
#19996=CARTESIAN_POINT('Ctrl Pts',(2.25180017160661,-1.66063371893121,11.0502777777778));
#19997=CARTESIAN_POINT('Ctrl Pts',(2.62205116590109,0.976297109112734,11.2081388888889));
#19998=CARTESIAN_POINT('Ctrl Pts',(0.617379419647229,2.72894686881467,11.366));
#19999=CARTESIAN_POINT('Ctrl Pts',(-1.9464837111559,2.00985310989732,11.5238611111111));
#20000=CARTESIAN_POINT('Ctrl Pts',(-2.74731929814685,-0.529665024907718,
11.6817222222222));
#20001=CARTESIAN_POINT('Ctrl Pts',(-1.05977053720295,-2.58943908287633,
11.8395833333333));
#20002=CARTESIAN_POINT('Ctrl Pts',(1.58766534266525,-2.30382879610199,11.9974444444444));
#20003=CARTESIAN_POINT('Ctrl Pts',(2.79707340746319,0.0684743370742143,
12.1553055555555));
#20004=CARTESIAN_POINT('Ctrl Pts',(1.47303233105958,2.37875683253439,12.3131666666667));
#20005=CARTESIAN_POINT('Ctrl Pts',(-1.18520769732058,2.53448043892505,12.4710277777778));
#20006=CARTESIAN_POINT('Ctrl Pts',(-2.76994594615232,0.394598452475193,
12.6288888888889));
#20007=CARTESIAN_POINT('Ctrl Pts',(-1.8458056761109,-2.1026909997905,12.78675));
#20008=CARTESIAN_POINT('Ctrl Pts',(0.750172845833004,-2.69546828972993,
12.9446111111111));
#20009=CARTESIAN_POINT('Ctrl Pts',(2.66668266040929,-0.846825037914988,
13.1024722222222));
#20010=CARTESIAN_POINT('Ctrl Pts',(2.16784415239069,1.76882949166842,13.2603333333333));
#20011=CARTESIAN_POINT('Ctrl Pts',(-0.294517949969841,2.78236767093066,
13.4181944444444));
#20012=CARTESIAN_POINT('Ctrl Pts',(-2.49012264935389,1.27577473748293,13.5760555555556));
#20013=CARTESIAN_POINT('Ctrl Pts',(-2.43029461870512,-1.3863478583448,13.7339166666666));
#20014=CARTESIAN_POINT('Ctrl Pts',(-0.16923542984156,-2.79279215602584,
13.8917777777778));
#20015=CARTESIAN_POINT('Ctrl Pts',(2.24512421134353,-1.66965318578134,14.0496388888889));
#20016=CARTESIAN_POINT('Ctrl Pts',(2.62593313585052,0.965751391486786,14.2075));
#20017=CARTESIAN_POINT('Ctrl Pts',(0.628359679142483,2.72647005025058,14.3653611111111));
#20018=CARTESIAN_POINT('Ctrl Pts',(-1.93845838021891,2.01760572163479,14.5232222222222));
#20019=CARTESIAN_POINT('Ctrl Pts',(-2.74931180160372,-0.518546638254714,
14.6810833333333));
#20020=CARTESIAN_POINT('Ctrl Pts',(-1.07036982067409,-2.58532778276268,
14.8389444444444));
#20021=CARTESIAN_POINT('Ctrl Pts',(1.57881200919325,-2.30987053095853,14.9968055555556));
#20022=CARTESIAN_POINT('Ctrl Pts',(2.79654399706859,0.0566462213665858,
15.1546666666667));
#20023=CARTESIAN_POINT('Ctrl Pts',(1.48409012818578,2.37398300468726,15.3125277777778));
#20024=CARTESIAN_POINT('Ctrl Pts',(-1.17817012667699,2.53688639776398,15.4703888888889));
#20025=CARTESIAN_POINT('Ctrl Pts',(-2.23297482288527,1.11978691060522,15.5756296296296));
#20026=CARTESIAN_POINT('Ctrl Pts',(-2.34668236863854,0.343918483395395,
15.62825));
#20027=CARTESIAN_POINT('',(1.37702479013102,-1.93106208855765,0.));
#20028=CARTESIAN_POINT('Ctrl Pts',(1.37702479013102,-1.93106208855765,-3.60822483003176E-15));
#20029=CARTESIAN_POINT('Ctrl Pts',(2.01547936988864,-1.47578528057288,0.0526203703703667));
#20030=CARTESIAN_POINT('Ctrl Pts',(2.79497483704674,0.109513025844136,0.157861111111108));
#20031=CARTESIAN_POINT('Ctrl Pts',(1.4349850222035,2.40398352764199,0.315722222222219));
#20032=CARTESIAN_POINT('Ctrl Pts',(-1.225925966736,2.51415445945906,0.473583333333329));
#20033=CARTESIAN_POINT('Ctrl Pts',(-2.32453883371355,0.980556500150706,
0.585479295290919));
#20034=CARTESIAN_POINT('Ctrl Pts',(-2.37485146083742,0.100616720091163,
0.644754886878137));
#20035=CARTESIAN_POINT('Ctrl Pts',(-2.37409249406917,0.00172857025301858,
0.651410108094986));
#20036=CARTESIAN_POINT('Ctrl Pts',(1.29200104020317,2.64812001020929,8.84708972748172E-17));
#20037=CARTESIAN_POINT('Ctrl Pts',(1.36315737313149,2.60529414881161,1.11522009070411E-16));
#20038=CARTESIAN_POINT('Ctrl Pts',(1.43224767624703,2.55934891308958,-5.0435019692162E-16));
#20039=CARTESIAN_POINT('Ctrl Pts',(1.49903325513988,2.51027466650741,-4.38885039422132E-16));
#20040=CARTESIAN_POINT('Ctrl Pts',(1.57786836962904,2.45234638450537,-3.65724347932505E-16));
#20041=CARTESIAN_POINT('Ctrl Pts',(1.65349331585608,2.39005818913334,-5.19266877679362E-16));
#20042=CARTESIAN_POINT('Ctrl Pts',(1.72573019513852,2.32378926839401,-6.48786580015326E-16));
#20043=CARTESIAN_POINT('Ctrl Pts',(1.76374109312884,2.28891869797108,-7.16939582223243E-16));
#20044=CARTESIAN_POINT('Ctrl Pts',(1.80081318017132,2.2529453987339,-5.63901193634668E-16));
#20045=CARTESIAN_POINT('Ctrl Pts',(1.83691551656788,2.21592189026143,-5.759281940243E-16));
#20046=CARTESIAN_POINT('Ctrl Pts',(1.85077163488616,2.20171222503873,-5.80544170635404E-16));
#20047=CARTESIAN_POINT('Ctrl Pts',(1.86448486767998,2.18734784556943,1.18680337545582E-16));
#20048=CARTESIAN_POINT('Ctrl Pts',(1.87805332095389,2.17283167229843,1.45716771982052E-16));
#20049=CARTESIAN_POINT('Ctrl Pts',(1.88973877018296,2.16033002584437,1.69001141656681E-16));
#20050=CARTESIAN_POINT('Ctrl Pts',(1.90131548250979,2.14771713833219,-1.20552840767492E-16));
#20051=CARTESIAN_POINT('Ctrl Pts',(1.91277473204616,2.1350036118777,-1.04083408558608E-16));
#20052=CARTESIAN_POINT('Ctrl Pts',(1.9778462733255,2.06280963801715,-1.05614606835039E-17));
#20053=CARTESIAN_POINT('Ctrl Pts',(2.03920496551099,1.98729716595704,-4.81412066085989E-16));
#20054=CARTESIAN_POINT('Ctrl Pts',(2.09668120715734,1.90884345828848,-3.33066907387547E-16));
#20055=CARTESIAN_POINT('Ctrl Pts',(2.14417843271961,1.84401087107344,-2.10477411937863E-16));
#20056=CARTESIAN_POINT('Ctrl Pts',(2.18902362087598,1.7771688452355,-1.7119245770294E-16));
#20057=CARTESIAN_POINT('Ctrl Pts',(2.23109606376114,1.7085204430367,-1.94289029309402E-16));
#20058=CARTESIAN_POINT('Ctrl Pts',(2.24950275752339,1.67848676707472,-2.0439377938723E-16));
#20059=CARTESIAN_POINT('Ctrl Pts',(2.26737842523222,1.6481072631063,-4.61788465798711E-16));
#20060=CARTESIAN_POINT('Ctrl Pts',(2.28471149018554,1.61739870311764,-5.13478148889135E-16));
#20061=CARTESIAN_POINT('Ctrl Pts',(2.29518347047447,1.59884575614786,-5.44707094486553E-16));
#20062=CARTESIAN_POINT('Ctrl Pts',(2.30545737670969,1.58017269818218,-5.13081578012294E-16));
#20063=CARTESIAN_POINT('Ctrl Pts',(2.3155304906665,1.56138322284078,-5.55111512312578E-16));
#20064=CARTESIAN_POINT('Ctrl Pts',(2.32274660107223,1.54792294341672,-5.85220637212436E-16));
#20065=CARTESIAN_POINT('Ctrl Pts',(2.32985933504635,1.5344033850802,-2.08590721469464E-17));
#20066=CARTESIAN_POINT('Ctrl Pts',(2.33686168047272,1.52083799385098,-2.77555756156289E-17));
#20067=CARTESIAN_POINT('Ctrl Pts',(2.38047027627073,1.43635663411551,-7.07050181056999E-17));
#20068=CARTESIAN_POINT('Ctrl Pts',(2.41986655819018,1.34997905359849,1.3198210981114E-16));
#20069=CARTESIAN_POINT('Ctrl Pts',(2.45488985599288,1.26205357875123,5.55111512312578E-17));
#20070=CARTESIAN_POINT('Ctrl Pts',(2.48959846523414,1.17491812491653,-2.02727065483809E-17));
#20071=CARTESIAN_POINT('Ctrl Pts',(2.52001253380174,1.08626153918075,-4.44579204063227E-16));
#20072=CARTESIAN_POINT('Ctrl Pts',(2.54592562425351,0.996413712953991,-4.9960036108132E-16));
#20073=CARTESIAN_POINT('Ctrl Pts',(2.57101139534936,0.909434430942866,-5.528648743571E-16));
#20074=CARTESIAN_POINT('Ctrl Pts',(2.59187898968551,0.821337996875181,-7.89241560757653E-18));
#20075=CARTESIAN_POINT('Ctrl Pts',(2.60829286172102,0.732427405689614,-8.32667268468867E-17));
#20076=CARTESIAN_POINT('Ctrl Pts',(2.61783087340729,0.680761945161682,-1.27066328786625E-16));
#20077=CARTESIAN_POINT('Ctrl Pts',(2.62586408863254,0.628821695636964,-4.14952786105416E-17));
#20078=CARTESIAN_POINT('Ctrl Pts',(2.63233843305125,0.576668196894126,-5.55111512312578E-17));
#20079=CARTESIAN_POINT('Ctrl Pts',(2.63414224296016,0.562137768524485,-5.94160979378542E-17));
#20080=CARTESIAN_POINT('Ctrl Pts',(2.63582527555606,0.547588319420663,3.76279563716787E-16));
#20081=CARTESIAN_POINT('Ctrl Pts',(2.63738542604938,0.533029261526728,3.60822483003176E-16));
#20082=CARTESIAN_POINT('Ctrl Pts',(2.64690685377435,0.444176924476997,2.66489610960485E-16));
#20083=CARTESIAN_POINT('Ctrl Pts',(2.65183263786108,0.355196731300303,5.62349138697447E-16));
#20084=CARTESIAN_POINT('Ctrl Pts',(2.65198717743404,0.266381980286723,3.88578058618805E-16));
#20085=CARTESIAN_POINT('Ctrl Pts',(2.65207998114243,0.213047173573617,2.84225494854879E-16));
#20086=CARTESIAN_POINT('Ctrl Pts',(2.65045121279133,0.159772024909719,-3.854419951949E-17));
#20087=CARTESIAN_POINT('Ctrl Pts',(2.64705383408491,0.106621318043217,-8.32667268468867E-17));
#20088=CARTESIAN_POINT('Ctrl Pts',(2.64128166054733,0.0163178428672467,
-1.29468843946197E-16));
#20089=CARTESIAN_POINT('Ctrl Pts',(2.63040647827402,-0.0736278476965388,
-4.84995897836269E-16));
#20090=CARTESIAN_POINT('Ctrl Pts',(2.61462343406994,-0.162881882998066,
-6.10622663543836E-16));
#20091=CARTESIAN_POINT('Ctrl Pts',(2.59852152905154,-0.253939094797703,
-7.38787434739808E-16));
#20092=CARTESIAN_POINT('Ctrl Pts',(2.57731092756958,-0.344277415185344,
-3.0810955291451E-16));
#20093=CARTESIAN_POINT('Ctrl Pts',(2.55115372858487,-0.433510589178544,
-3.60822483003176E-16));
#20094=CARTESIAN_POINT('Ctrl Pts',(2.54730992415644,-0.446623417870874,
-3.68568656216471E-16));
#20095=CARTESIAN_POINT('Ctrl Pts',(2.54335838534963,-0.4597150170452,-1.33461876853334E-16));
#20096=CARTESIAN_POINT('Ctrl Pts',(2.53930241226215,-0.472774949708627,
-1.38777878078145E-16));
#20097=CARTESIAN_POINT('Ctrl Pts',(2.51300579541719,-0.557448106523011,
-1.73243798916645E-16));
#20098=CARTESIAN_POINT('Ctrl Pts',(2.48237490705721,-0.640633082262047,
2.2266366763076E-16));
#20099=CARTESIAN_POINT('Ctrl Pts',(2.4476284488952,-0.722031078376524,1.66533453693773E-16));
#20100=CARTESIAN_POINT('Ctrl Pts',(2.41285997251409,-0.803480654968775,
1.10367671027941E-16));
#20101=CARTESIAN_POINT('Ctrl Pts',(2.37397005509887,-0.883141781461701,
-2.60473824643759E-16));
#20102=CARTESIAN_POINT('Ctrl Pts',(2.33113438836321,-0.960686402199183,
-2.22044604925031E-16));
#20103=CARTESIAN_POINT('Ctrl Pts',(2.28891526223189,-1.03711491080453,-1.84168503113759E-16));
#20104=CARTESIAN_POINT('Ctrl Pts',(2.24286247138705,-1.11148803969701,-4.86311355035046E-16));
#20105=CARTESIAN_POINT('Ctrl Pts',(2.19311210725222,-1.18345333925267,-6.10622663543836E-16));
#20106=CARTESIAN_POINT('Ctrl Pts',(2.16658994742807,-1.22181838863071,-6.76893623556989E-16));
#20107=CARTESIAN_POINT('Ctrl Pts',(2.13901644812981,-1.25949841963374,-1.03661145615814E-16));
#20108=CARTESIAN_POINT('Ctrl Pts',(2.11040940583919,-1.29643454206688,-5.55111512312578E-17));
#20109=CARTESIAN_POINT('Ctrl Pts',(2.10166865720486,-1.30772020237512,-4.0799144537779E-17));
#20110=CARTESIAN_POINT('Ctrl Pts',(2.09283023898332,-1.31893783850973,-3.98702450321844E-16));
#20111=CARTESIAN_POINT('Ctrl Pts',(2.08389831377262,-1.33008110200649,-3.88578058618805E-16));
#20112=CARTESIAN_POINT('Ctrl Pts',(2.03043260129099,-1.39678368942974,-3.27974347428123E-16));
#20113=CARTESIAN_POINT('Ctrl Pts',(1.97380215986925,-1.46059813131217,-2.08556400160018E-16));
#20114=CARTESIAN_POINT('Ctrl Pts',(1.91417150281915,-1.52123259912064,-1.11022302462516E-16));
#20115=CARTESIAN_POINT('Ctrl Pts',(1.85542332105702,-1.58096973622562,-1.49316138302572E-17));
#20116=CARTESIAN_POINT('Ctrl Pts',(1.79376241718216,-1.63762085789259,-5.35520206863283E-16));
#20117=CARTESIAN_POINT('Ctrl Pts',(1.72931881925135,-1.69086532717403,-5.55111512312578E-16));
#20118=CARTESIAN_POINT('Ctrl Pts',(1.66690919772329,-1.7424292882658,-5.74084474679515E-16));
#20119=CARTESIAN_POINT('Ctrl Pts',(1.60188918190129,-1.79079854027645,-4.05239810717764E-16));
#20120=CARTESIAN_POINT('Ctrl Pts',(1.53436012060039,-1.83563678794726,-4.44089209850063E-16));
#20121=CARTESIAN_POINT('Ctrl Pts',(1.48333459704145,-1.8695169429323,-4.73444140786276E-16));
#20122=CARTESIAN_POINT('Ctrl Pts',(1.43087616732457,-1.90138023485661,-2.26823314612322E-16));
#20123=CARTESIAN_POINT('Ctrl Pts',(1.37702479013106,-1.93106208855762,-2.22044604925031E-16));
#20124=CARTESIAN_POINT('Ctrl Pts',(0.260984867623806,2.92515103163649,15.058));
#20125=CARTESIAN_POINT('Ctrl Pts',(0.721611965671866,2.88493263312463,15.0330979289241));
#20126=CARTESIAN_POINT('Ctrl Pts',(1.17298362662806,2.74202417939443,15.0081958578483));
#20127=CARTESIAN_POINT('Ctrl Pts',(1.56185858228333,2.49936439089571,14.9832937867724));
#20128=CARTESIAN_POINT('Ctrl Pts',(2.3835871899963,1.98660190194863,14.930673416402));
#20129=CARTESIAN_POINT('Ctrl Pts',(2.92625811262771,1.02843390833919,14.8780530460316));
#20130=CARTESIAN_POINT('Ctrl Pts',(2.94584082398175,0.0600984948350938,
14.8254326756613));
#20131=CARTESIAN_POINT('Ctrl Pts',(2.96542353533579,-0.90823691866899,14.7728123052909));
#20132=CARTESIAN_POINT('Ctrl Pts',(2.46191803541247,-1.88673975206773,14.7201919349205));
#20133=CARTESIAN_POINT('Ctrl Pts',(1.6624759601657,-2.43293893833301,14.6675715645502));
#20134=CARTESIAN_POINT('Ctrl Pts',(0.863033884918936,-2.97913812459828,
14.6149511941798));
#20135=CARTESIAN_POINT('Ctrl Pts',(-0.232344765651281,-3.0930336637301,
14.5623308238094));
#20136=CARTESIAN_POINT('Ctrl Pts',(-1.12713695505886,-2.72269707033318,
14.5097104534391));
#20137=CARTESIAN_POINT('Ctrl Pts',(-2.02192914446644,-2.35236047693625,
14.4570900830687));
#20138=CARTESIAN_POINT('Ctrl Pts',(-2.71613487271139,-1.49779175101059,
14.4044697126983));
#20139=CARTESIAN_POINT('Ctrl Pts',(-2.89560267371491,-0.546185667602603,
14.351849342328));
#20140=CARTESIAN_POINT('Ctrl Pts',(-2.9293373183321,-0.367311836977727,
14.3419582672485));
#20141=CARTESIAN_POINT('Ctrl Pts',(-2.94488478294563,-0.185009395803266,
14.3320671921691));
#20142=CARTESIAN_POINT('Ctrl Pts',(-2.94325266537063,-0.0024318079996577,
14.3221761170896));
#20143=CARTESIAN_POINT('Origin',(0.,0.,-1.84858989190501));
#20144=CARTESIAN_POINT('',(-1.37702479013098,-1.93106208855768,0.));
#20145=CARTESIAN_POINT('Ctrl Pts',(-1.37994859234593,-1.93347131995891,
-1.03866568124111E-15));
#20146=CARTESIAN_POINT('Ctrl Pts',(-0.794305021574331,-2.34617453422284,
0.0482502273315914));
#20147=CARTESIAN_POINT('Ctrl Pts',(0.853330802601401,-2.62819893329841,
0.149165418329868));
#20148=CARTESIAN_POINT('Ctrl Pts',(2.68321992772198,-0.795544356782894,
0.30274557299483));
#20149=CARTESIAN_POINT('Ctrl Pts',(2.13222685489998,1.81318819272267,0.460740463994884));
#20150=CARTESIAN_POINT('Ctrl Pts',(-0.353356050373597,2.77617865909866,
0.618735354994938));
#20151=CARTESIAN_POINT('Ctrl Pts',(-2.12480812784407,1.50378450145058,0.74801849763165));
#20152=CARTESIAN_POINT('Ctrl Pts',(-2.36883710346974,0.358840951777969,
0.824636676601679));
#20153=CARTESIAN_POINT('Ctrl Pts',(-2.36806791026422,0.000580996437929554,
0.848589891905023));
#20154=CARTESIAN_POINT('Origin',(0.,0.,0.));
#20155=CARTESIAN_POINT('Ctrl Pts',(-1.03908919352511,2.13201587949043,-0.329233991005384));
#20156=CARTESIAN_POINT('Ctrl Pts',(-1.74458119175558,1.78817739379635,-0.2765690273387));
#20157=CARTESIAN_POINT('Ctrl Pts',(-2.77573338088225,0.351504794741619,
-0.171239100005331));
#20158=CARTESIAN_POINT('Ctrl Pts',(-1.80933791412281,-2.1375423700464,-0.013244209005277));
#20159=CARTESIAN_POINT('Ctrl Pts',(0.800729748594893,-2.68087948155196,
0.144750681994776));
#20160=CARTESIAN_POINT('Ctrl Pts',(2.68321992772198,-0.795544356782894,
0.30274557299483));
#20161=CARTESIAN_POINT('Ctrl Pts',(2.13222685489998,1.81318819272267,0.460740463994884));
#20162=CARTESIAN_POINT('Ctrl Pts',(-0.353356050373597,2.77617865909866,
0.618735354994938));
#20163=CARTESIAN_POINT('Ctrl Pts',(-2.51821971460423,1.2212058130903,0.77673024599499));
#20164=CARTESIAN_POINT('Ctrl Pts',(-2.39875016986203,-1.44183805604875,
0.934725136995045));
#20165=CARTESIAN_POINT('Ctrl Pts',(-0.103189861818606,-2.79677945469355,
1.0927200279951));
#20166=CARTESIAN_POINT('Ctrl Pts',(2.28595558559378,-1.6146683983646,1.25071491899515));
#20167=CARTESIAN_POINT('Ctrl Pts',(2.60139192527736,1.0322363870214,1.4087098099952));
#20168=CARTESIAN_POINT('Ctrl Pts',(0.556949311928898,2.7427217714679,1.56670470099526));
#20169=CARTESIAN_POINT('Ctrl Pts',(-1.99273057992189,1.96513605211958,1.72469959199531));
#20170=CARTESIAN_POINT('Ctrl Pts',(-2.73469173326279,-0.595142683011921,
1.88269448299537));
#20171=CARTESIAN_POINT('Ctrl Pts',(-0.995855715555496,-2.61553061219188,
2.04068937399542));
#20172=CARTESIAN_POINT('Ctrl Pts',(1.64637781974439,-2.26322161422709,2.19868426499547));
#20173=CARTESIAN_POINT('Ctrl Pts',(2.79508756969503,0.142186649832604,2.35667915599553));
#20174=CARTESIAN_POINT('Ctrl Pts',(1.40821242874264,2.41860884498944,2.51467404699558));
#20175=CARTESIAN_POINT('Ctrl Pts',(-1.25613315819632,2.50097199645567,2.67266893799564));
#20176=CARTESIAN_POINT('Ctrl Pts',(-2.78096812139655,0.314559449318749,
2.83066382899569));
#20177=CARTESIAN_POINT('Ctrl Pts',(-1.78302687496254,-2.15720801874703,
2.98865871999574));
#20178=CARTESIAN_POINT('Ctrl Pts',(0.832400628534772,-2.67204800324426,
3.1466536109958));
#20179=CARTESIAN_POINT('Ctrl Pts',(2.69270963387839,-0.762919488957052,
3.30464850199585));
#20180=CARTESIAN_POINT('Ctrl Pts',(2.11030679852043,1.83829718168443,3.4626433929959));
#20181=CARTESIAN_POINT('Ctrl Pts',(-0.386476751895552,2.77188871376435,
3.62063828399595));
#20182=CARTESIAN_POINT('Ctrl Pts',(-2.53266500493224,1.1909405067813,3.77863317499601));
#20183=CARTESIAN_POINT('Ctrl Pts',(-2.38132711099884,-1.47037835529628,
3.93662806599605));
#20184=CARTESIAN_POINT('Ctrl Pts',(-0.0697503817448946,-2.79783241149437,
4.09462295699612));
#20185=CARTESIAN_POINT('Ctrl Pts',(2.30510093209087,-1.58721170953314,4.25261784799616));
#20186=CARTESIAN_POINT('Ctrl Pts',(2.5888625630092,1.06326005653742,4.41061273899623));
#20187=CARTESIAN_POINT('Ctrl Pts',(0.524118009051023,2.74918744918107,4.56860762999628));
#20188=CARTESIAN_POINT('Ctrl Pts',(-2.01608414683087,1.9411687281004,4.72660252099633));
#20189=CARTESIAN_POINT('Ctrl Pts',(-2.72738037475851,-0.627795834204506,
4.88459741199638));
#20190=CARTESIAN_POINT('Ctrl Pts',(-0.964512940920624,-2.62725067416123,
5.04259230299644));
#20191=CARTESIAN_POINT('Ctrl Pts',(1.67331967629405,-2.24337526486265,5.20058719399648));
#20192=CARTESIAN_POINT('Ctrl Pts',(2.79318773824162,0.175594923072764,5.35858208499656));
#20193=CARTESIAN_POINT('Ctrl Pts',(1.37919449268132,2.43527285317938,5.51657697599659));
#20194=CARTESIAN_POINT('Ctrl Pts',(-1.28594543116668,2.48577466117395,5.67457186699666));
#20195=CARTESIAN_POINT('Ctrl Pts',(-2.78453026564846,0.281287251330417,
5.8325667579967));
#20196=CARTESIAN_POINT('Ctrl Pts',(-1.75710748413146,-2.17837200846936,
5.99056164899676));
#20197=CARTESIAN_POINT('Ctrl Pts',(0.864288593995119,-2.66190468356086,
6.14855653999681));
#20198=CARTESIAN_POINT('Ctrl Pts',(2.70163876039796,-0.730670463607777,
6.30655143099686));
#20199=CARTESIAN_POINT('Ctrl Pts',(2.08817696449889,1.86339697407977,6.46454632199692));
#20200=CARTESIAN_POINT('Ctrl Pts',(-0.419590302218696,2.76706980330411,
6.62254121299697));
#20201=CARTESIAN_POINT('Ctrl Pts',(-2.54672306405081,1.16057440653543,6.78053610399702));
#20202=CARTESIAN_POINT('Ctrl Pts',(-2.3635768050391,-1.49874480975067,6.93853099499709));
#20203=CARTESIAN_POINT('Ctrl Pts',(-0.0362940343214689,-2.79846637663312,
7.09652588599712));
#20204=CARTESIAN_POINT('Ctrl Pts',(2.32391314315961,-1.55953807940794,7.2545207769972));
#20205=CARTESIAN_POINT('Ctrl Pts',(2.57596499873257,1.09413693995685,7.41251566799723));
#20206=CARTESIAN_POINT('Ctrl Pts',(0.491210792034311,2.75525738831465,7.5705105589973));
#20207=CARTESIAN_POINT('Ctrl Pts',(-2.03914898665099,1.91692533196097,7.72850544999735));
#20208=CARTESIAN_POINT('Ctrl Pts',(-2.71967939412015,-0.66035998612245,
7.8865003409974));
#20209=CARTESIAN_POINT('Ctrl Pts',(-0.9330321424437,-2.63859476601473,8.04449523199746));
#20210=CARTESIAN_POINT('Ctrl Pts',(1.70002224901497,-2.22320841823872,8.2024901229975));
#20211=CARTESIAN_POINT('Ctrl Pts',(2.79088864512093,0.208978201275766,8.36048501399757));
#20212=CARTESIAN_POINT('Ctrl Pts',(1.34997937336987,2.45158867054595,8.51847990499762));
#20213=CARTESIAN_POINT('Ctrl Pts',(-1.31557386100644,2.47022200101732,8.67647479599767));
#20214=CARTESIAN_POINT('Ctrl Pts',(-2.78769435259396,0.247974826523285,
8.83446968699772));
#20215=CARTESIAN_POINT('Ctrl Pts',(-1.73093690286391,-2.19922458070505,
8.99246457799778));
#20216=CARTESIAN_POINT('Ctrl Pts',(0.896053003445084,-2.6513808351669,9.15045946899784));
#20217=CARTESIAN_POINT('Ctrl Pts',(2.71018167460651,-0.698316982967359,
9.30845435999788));
#20218=CARTESIAN_POINT('Ctrl Pts',(2.06574861445826,1.88823038317285,9.46644925099794));
#20219=CARTESIAN_POINT('Ctrl Pts',(-0.45264386973844,2.76185532663481,9.62444414199799));
#20220=CARTESIAN_POINT('Ctrl Pts',(-2.5604170561675,1.13004239591331,9.78243903299804));
#20221=CARTESIAN_POINT('Ctrl Pts',(-2.34548861359897,-1.52689701078686,
9.9404339239981));
#20222=CARTESIAN_POINT('Ctrl Pts',(-0.00283249851198579,-2.79870028674429,
10.0984288149982));
#20223=CARTESIAN_POINT('Ctrl Pts',(2.34239313895008,-1.53164150527581,10.2564237059982));
#20224=CARTESIAN_POINT('Ctrl Pts',(2.56269918704329,1.12485741087042,10.4144185969983));
#20225=CARTESIAN_POINT('Ctrl Pts',(0.458233353927178,2.76093344928963,10.5724134879983));
#20226=CARTESIAN_POINT('Ctrl Pts',(-2.06192231968409,1.89240790151988,10.7304083789984));
#20227=CARTESIAN_POINT('Ctrl Pts',(-2.71158962134898,-0.692829736205835,
10.8884032699984));
#20228=CARTESIAN_POINT('Ctrl Pts',(-0.90141796228012,-2.64956165719617,
11.0463981609985));
#20229=CARTESIAN_POINT('Ctrl Pts',(1.72648179491819,-2.20272375262492,11.2043930519985));
#20230=CARTESIAN_POINT('Ctrl Pts',(2.7881905800153,0.242331605070017,11.3623879429986));
#20231=CARTESIAN_POINT('Ctrl Pts',(1.32057126786748,2.46755402056041,11.5203828339987));
#20232=CARTESIAN_POINT('Ctrl Pts',(-1.34501422335496,2.45431621031658,11.6783777249987));
#20233=CARTESIAN_POINT('Ctrl Pts',(-2.79045992331823,0.214626951768239,
11.8363726159988));
#20234=CARTESIAN_POINT('Ctrl Pts',(-1.70451887724915,-2.21976276122321,
11.9943675069988));
#20235=CARTESIAN_POINT('Ctrl Pts',(0.927689321261817,-2.64047796075702,
12.1523623979988));
#20236=CARTESIAN_POINT('Ctrl Pts',(2.71833714731268,-0.66586366962402,12.3103572889989));
#20237=CARTESIAN_POINT('Ctrl Pts',(2.04302496870488,1.91279385105346,12.468352179999));
#20238=CARTESIAN_POINT('Ctrl Pts',(-0.48563275555883,2.75624604578475,12.626347070999));
#20239=CARTESIAN_POINT('Ctrl Pts',(-2.57374497374716,1.09934880708429,12.7843419619991));
#20240=CARTESIAN_POINT('Ctrl Pts',(-2.32706521767492,-1.55483087129818,
12.9423368529991));
#20241=CARTESIAN_POINT('Ctrl Pts',(0.0306296239850783,-2.7985342282319,
13.1003317439992));
#20242=CARTESIAN_POINT('Ctrl Pts',(2.36053793034993,-1.50352574600393,13.2583266349992));
#20243=CARTESIAN_POINT('Ctrl Pts',(2.54906768788899,1.15541663986578,13.4163215259993));
#20244=CARTESIAN_POINT('Ctrl Pts',(0.42518914129335,2.76621565710669,13.5743164169993));
#20245=CARTESIAN_POINT('Ctrl Pts',(-2.08439846825039,1.86761834358563,13.7323113079994));
#20246=CARTESIAN_POINT('Ctrl Pts',(-2.7031168406022,-0.725197389434075,
13.8903061989994));
#20247=CARTESIAN_POINT('Ctrl Pts',(-0.869666078203209,-2.66015561356989,
14.0483010899995));
#20248=CARTESIAN_POINT('Ctrl Pts',(1.75267763866885,-2.18191305067097,14.2062959809995));
#20249=CARTESIAN_POINT('Ctrl Pts',(2.78512620401791,0.275629071355557,14.3642908719996));
#20250=CARTESIAN_POINT('Ctrl Pts',(1.29091271455523,2.48320730756548,14.5222857629997));
#20251=CARTESIAN_POINT('Ctrl Pts',(-1.37414448785656,2.43798182357128,14.6802806539997));
#20252=CARTESIAN_POINT('Ctrl Pts',(-2.79305172314729,0.181396953694044,
14.8382755449998));
#20253=CARTESIAN_POINT('Ctrl Pts',(-1.67742675687761,-2.24026772494819,
14.9962704359998));
#20254=CARTESIAN_POINT('Ctrl Pts',(0.958368222991996,-2.62865236842956,
15.1542653269999));
#20255=CARTESIAN_POINT('Ctrl Pts',(2.7277014223945,-0.634378452891388,15.3122602179999));
#20256=CARTESIAN_POINT('Ctrl Pts',(2.01676643438217,1.93930517753648,15.470255109));
#20257=CARTESIAN_POINT('Ctrl Pts',(0.331786659212352,2.47609764328476,15.5755850363333));
#20258=CARTESIAN_POINT('Ctrl Pts',(-0.439445221994538,2.33068358199181,
15.62825));
#20259=CARTESIAN_POINT('Ctrl Pts',(-1.12236674703448,2.30288577939268,-0.219489327336923));
#20260=CARTESIAN_POINT('Ctrl Pts',(-1.88440023178909,1.93149044095738,-0.166824363670239));
#20261=CARTESIAN_POINT('Ctrl Pts',(-2.99819386511655,0.37967606197771,-0.0614944363368692));
#20262=CARTESIAN_POINT('Ctrl Pts',(-1.9543468660962,-2.30885518920509,0.096500454663184));
#20263=CARTESIAN_POINT('Ctrl Pts',(0.864904041716857,-2.89573792283723,
0.254495345663238));
#20264=CARTESIAN_POINT('Ctrl Pts',(2.89826594350265,-0.859303067925248,
0.412490236663291));
#20265=CARTESIAN_POINT('Ctrl Pts',(2.30311366337569,1.95850572434841,0.570485127663346));
#20266=CARTESIAN_POINT('Ctrl Pts',(-0.381675686047029,2.99867483004853,
0.728480018663398));
#20267=CARTESIAN_POINT('Ctrl Pts',(-2.72004182798788,1.31907905927489,0.886474909663454));
#20268=CARTESIAN_POINT('Ctrl Pts',(-2.59099742531531,-1.55739382028214,
1.0444698006635));
#20269=CARTESIAN_POINT('Ctrl Pts',(-0.111459988476451,-3.02092667145178,
1.20246469166356));
#20270=CARTESIAN_POINT('Ctrl Pts',(2.46916294621846,-1.74407560881646,1.36045958266361));
#20271=CARTESIAN_POINT('Ctrl Pts',(2.80987985548213,1.11496472400166,1.51845447366367));
#20272=CARTESIAN_POINT('Ctrl Pts',(0.60158588058462,2.96253654820512,1.67644936466372));
#20273=CARTESIAN_POINT('Ctrl Pts',(-2.15243749298894,2.12263140839256,1.83444425566377));
#20274=CARTESIAN_POINT('Ctrl Pts',(-2.95386294451934,-0.642840250207365,
1.99243914666383));
#20275=CARTESIAN_POINT('Ctrl Pts',(-1.07566833237088,-2.82515168405898,
2.15043403766388));
#20276=CARTESIAN_POINT('Ctrl Pts',(1.77832637414643,-2.44460696618424,2.30842892866393));
#20277=CARTESIAN_POINT('Ctrl Pts',(3.01909919073696,0.153582164686878,2.46642381966399));
#20278=CARTESIAN_POINT('Ctrl Pts',(1.52107327516274,2.61244766918467,2.62441871066404));
#20279=CARTESIAN_POINT('Ctrl Pts',(-1.35680564805421,2.70141179561648,2.7824136016641));
#20280=CARTESIAN_POINT('Ctrl Pts',(-3.00384814265038,0.339769740731444,
2.94040849266415));
#20281=CARTESIAN_POINT('Ctrl Pts',(-1.92592713503036,-2.33009693659115,
3.0984033836642));
#20282=CARTESIAN_POINT('Ctrl Pts',(0.899113176712534,-2.88619864782458,
3.25639827466426));
#20283=CARTESIAN_POINT('Ctrl Pts',(2.90851619987664,-0.824063487913928,
3.41439316566431));
#20284=CARTESIAN_POINT('Ctrl Pts',(2.27943682934948,1.98562706719167,3.57238805666436));
#20285=CARTESIAN_POINT('Ctrl Pts',(-0.417450838226782,2.99404106807715,
3.73038294766441));
#20286=CARTESIAN_POINT('Ctrl Pts',(-2.73564483263507,1.2863881472707,3.88837783866447));
#20287=CARTESIAN_POINT('Ctrl Pts',(-2.57217799958985,-1.5882214749488,4.04637272966452));
#20288=CARTESIAN_POINT('Ctrl Pts',(-0.0753405093145775,-3.02206401722216,
4.20436762066458));
#20289=CARTESIAN_POINT('Ctrl Pts',(2.48984269190601,-1.71441841026206,4.36236251166463));
#20290=CARTESIAN_POINT('Ctrl Pts',(2.79634633048836,1.1484747780497,4.52035740266469));
#20291=CARTESIAN_POINT('Ctrl Pts',(0.566123320833673,2.9695204161036,4.67835229366474));
#20292=CARTESIAN_POINT('Ctrl Pts',(-2.1776627259012,2.09674322895411,4.83634718466479));
#20293=CARTESIAN_POINT('Ctrl Pts',(-2.94596561894615,-0.678110380349046,
4.99434207566485));
#20294=CARTESIAN_POINT('Ctrl Pts',(-1.04181359860098,-2.83781104757613,
5.1523369666649));
#20295=CARTESIAN_POINT('Ctrl Pts',(1.80742747930962,-2.42317003592312,5.31033185766495));
#20296=CARTESIAN_POINT('Ctrl Pts',(3.01704709774863,0.189667935951029,5.46832674866501));
#20297=CARTESIAN_POINT('Ctrl Pts',(1.48972970359473,2.63044721030322,5.62632163966506));
#20298=CARTESIAN_POINT('Ctrl Pts',(-1.38900721847178,2.68499647355363,5.78431653066512));
#20299=CARTESIAN_POINT('Ctrl Pts',(-3.00769577409666,0.303830950437453,
5.94231142166516));
#20300=CARTESIAN_POINT('Ctrl Pts',(-1.89793044085485,-2.35295710917974,
6.10030631266523));
#20301=CARTESIAN_POINT('Ctrl Pts',(0.933556795495496,-2.87524239422467,
6.25830120366527));
#20302=CARTESIAN_POINT('Ctrl Pts',(2.91816094909363,-0.789229872184075,
6.41629609466533));
#20303=CARTESIAN_POINT('Ctrl Pts',(2.25553340510261,2.01273847641193,6.57429098566538));
#20304=CARTESIAN_POINT('Ctrl Pts',(-0.453218266076613,2.98883594719704,
6.73228587666544));
#20305=CARTESIAN_POINT('Ctrl Pts',(-2.75082957152067,1.25358836322381,6.89028076766548));
#20306=CARTESIAN_POINT('Ctrl Pts',(-2.55300509962799,-1.61886135207317,
7.04827565866555));
#20307=CARTESIAN_POINT('Ctrl Pts',(-0.0392028109733089,-3.02274879134448,
7.20627054966559));
#20308=CARTESIAN_POINT('Ctrl Pts',(2.51016260310644,-1.68452688370611,7.36426544066566));
#20309=CARTESIAN_POINT('Ctrl Pts',(2.78241509402469,1.18182628186475,7.5222603316657));
#20310=CARTESIAN_POINT('Ctrl Pts',(0.530578762823495,2.97607682904918,7.68025522266576));
#20311=CARTESIAN_POINT('Ctrl Pts',(-2.2025760917615,2.07055685166173,7.83825011366581));
#20312=CARTESIAN_POINT('Ctrl Pts',(-2.93764744506665,-0.713284378390626,
7.99624500466586));
#20313=CARTESIAN_POINT('Ctrl Pts',(-1.0078097791014,-2.85006430894292,8.15423989566592));
#20314=CARTESIAN_POINT('Ctrl Pts',(1.83627012329917,-2.40138692222673,8.31223478666596));
#20315=CARTESIAN_POINT('Ctrl Pts',(3.01456374436274,0.225726708956776,8.47022967766603));
#20316=CARTESIAN_POINT('Ctrl Pts',(1.45817314557243,2.64807065492862,8.62822456866608));
#20317=CARTESIAN_POINT('Ctrl Pts',(-1.42101021169528,2.66819734918923,8.78621945966612));
#20318=CARTESIAN_POINT('Ctrl Pts',(-3.01111344602942,0.267848709355943,
8.9442143506662));
#20319=CARTESIAN_POINT('Ctrl Pts',(-1.86966242464576,-2.37548090580212,
9.10220924166623));
#20320=CARTESIAN_POINT('Ctrl Pts',(0.967866955901341,-2.86387511453221,
9.26020413266631));
#20321=CARTESIAN_POINT('Ctrl Pts',(2.92738853310682,-0.754283429618888,
9.41819902366633));
#20322=CARTESIAN_POINT('Ctrl Pts',(2.23130754034209,2.03956215310421,9.57619391466641));
#20323=CARTESIAN_POINT('Ctrl Pts',(-0.488920903815691,2.98320355754919,
9.73418880566644));
#20324=CARTESIAN_POINT('Ctrl Pts',(-2.76562106534208,1.22060937195346,9.89218369666651));
#20325=CARTESIAN_POINT('Ctrl Pts',(-2.53346723443519,-1.64926980449067,
10.0501785876666));
#20326=CARTESIAN_POINT('Ctrl Pts',(-0.00305950842402692,-3.02300144812525,
10.2081734786666));
#20327=CARTESIAN_POINT('Ctrl Pts',(2.53012367371502,-1.65439454534941,10.3661683696667));
#20328=CARTESIAN_POINT('Ctrl Pts',(2.76808609704807,1.21500883753128,10.5241632606667));
#20329=CARTESIAN_POINT('Ctrl Pts',(0.494958355870487,2.98220779656589,10.6821581516668));
#20330=CARTESIAN_POINT('Ctrl Pts',(-2.22717458809345,2.0440744776545,10.8401530426668));
#20331=CARTESIAN_POINT('Ctrl Pts',(-2.92890931940236,-0.748356408785326,
10.9981479336669));
#20332=CARTESIAN_POINT('Ctrl Pts',(-0.973661888071959,-2.86191013898051,
11.1561428246669));
#20333=CARTESIAN_POINT('Ctrl Pts',(1.86485026314516,-2.37926051801397,11.314137715667));
#20334=CARTESIAN_POINT('Ctrl Pts',(3.01164944347811,0.261753213276476,11.472132606667));
#20335=CARTESIAN_POINT('Ctrl Pts',(1.42640813452734,2.66531554408024,11.6301274976671));
#20336=CARTESIAN_POINT('Ctrl Pts',(-1.45281006480367,2.6510167927182,11.7881223886671));
#20337=CARTESIAN_POINT('Ctrl Pts',(-3.01410066275426,0.231828177198969,
11.9461172796672));
#20338=CARTESIAN_POINT('Ctrl Pts',(-1.84112713272175,-2.39766511385838,
12.1041121706673));
#20339=CARTESIAN_POINT('Ctrl Pts',(1.00203875880082,-2.85209843187493,12.2621070616673));
#20340=CARTESIAN_POINT('Ctrl Pts',(2.9361976242116,-0.71922915328282,12.4201019526674));
#20341=CARTESIAN_POINT('Ctrl Pts',(2.20676271346495,2.0660942542105,12.5780968436674));
#20342=CARTESIAN_POINT('Ctrl Pts',(-0.52455367595618,2.97714472223446,12.7360917346675));
#20343=CARTESIAN_POINT('Ctrl Pts',(-2.78001714567073,1.1874558528297,12.8940866256675));
#20344=CARTESIAN_POINT('Ctrl Pts',(-2.51356729987571,-1.67944241753446,
13.0520815166676));
#20345=CARTESIAN_POINT('Ctrl Pts',(0.0330844278327718,-3.02282208089334,
13.2100764076676));
#20346=CARTESIAN_POINT('Ctrl Pts',(2.5497226750577,-1.62402545531265,13.3680712986677));
#20347=CARTESIAN_POINT('Ctrl Pts',(2.75336210467249,1.24801722858484,13.5260661896677));
#20348=CARTESIAN_POINT('Ctrl Pts',(0.459265822762407,2.98791334565805,13.6840610806678));
#20349=CARTESIAN_POINT('Ctrl Pts',(-2.25145208218098,2.01729816656161,13.8420559716679));
#20350=CARTESIAN_POINT('Ctrl Pts',(-2.91975748968037,-0.78331815979697,
14.0000508626679));
#20351=CARTESIAN_POINT('Ctrl Pts',(-0.939365256882179,-2.87335314543991,
14.158045753668));
#20352=CARTESIAN_POINT('Ctrl Pts',(1.893145566493,-2.35678194735699,14.316040644668));
#20353=CARTESIAN_POINT('Ctrl Pts',(3.0083394738034,0.297719296989276,14.4740355356681));
#20354=CARTESIAN_POINT('Ctrl Pts',(1.3943726035929,2.68222336000765,14.6320304266681));
#20355=CARTESIAN_POINT('Ctrl Pts',(-1.4842749673478,2.63337329047569,14.7900253176682));
#20356=CARTESIAN_POINT('Ctrl Pts',(-3.01690018175728,0.195934968921086,
14.9480202086682));
#20357=CARTESIAN_POINT('Ctrl Pts',(-1.81186372087882,-2.41981344296957,
15.1060150996683));
#20358=CARTESIAN_POINT('Ctrl Pts',(1.03517641373175,-2.8393250802945,15.2640099906683));
#20359=CARTESIAN_POINT('Ctrl Pts',(2.94631239686769,-0.685220561427491,
15.4220048816684));
#20360=CARTESIAN_POINT('Ctrl Pts',(2.17839969522424,2.09473032457841,15.5799997726684));
#20361=CARTESIAN_POINT('Ctrl Pts',(0.358377621218746,2.67454389339306,15.6853297000018));
#20362=CARTESIAN_POINT('Ctrl Pts',(-0.474664453622694,2.51747565713054,
15.7379946636685));
#20363=CARTESIAN_POINT('Ctrl Pts',(-1.20564430054385,2.47375567929493,-0.109744663668462));
#20364=CARTESIAN_POINT('Ctrl Pts',(-2.02421927182262,2.0748034881184,-0.057079700001777));
#20365=CARTESIAN_POINT('Ctrl Pts',(-3.22065434935084,0.407847329213798,
0.0482502273315919));
#20366=CARTESIAN_POINT('Ctrl Pts',(-2.09935581806959,-2.48016800836378,
0.206245118331646));
#20367=CARTESIAN_POINT('Ctrl Pts',(0.929078334838823,-3.11059636412251,
0.364240009331699));
#20368=CARTESIAN_POINT('Ctrl Pts',(3.11331195928332,-0.923061779067598,
0.522234900331752));
#20369=CARTESIAN_POINT('Ctrl Pts',(2.4740004718514,2.10382325597413,0.680229791331807));
#20370=CARTESIAN_POINT('Ctrl Pts',(-0.409995321720456,3.2211710009984,0.83822468233186));
#20371=CARTESIAN_POINT('Ctrl Pts',(-2.92186394137152,1.41695230545948,0.996219573331913));
#20372=CARTESIAN_POINT('Ctrl Pts',(-2.78324468076858,-1.67294958451553,
1.15421446433197));
#20373=CARTESIAN_POINT('Ctrl Pts',(-0.119730115134298,-3.24507388821001,
1.31220935533202));
#20374=CARTESIAN_POINT('Ctrl Pts',(2.65237030684314,-1.87348281926831,1.47020424633207));
#20375=CARTESIAN_POINT('Ctrl Pts',(3.0183677856869,1.19769306098192,1.62819913733213));
#20376=CARTESIAN_POINT('Ctrl Pts',(0.646222449240343,3.18235132494235,1.78619402833218));
#20377=CARTESIAN_POINT('Ctrl Pts',(-2.31214440605599,2.28012676466554,1.94418891933223));
#20378=CARTESIAN_POINT('Ctrl Pts',(-3.17303415577589,-0.690537817402807,
2.10218381033229));
#20379=CARTESIAN_POINT('Ctrl Pts',(-1.15548094918627,-3.03477275592607,
2.26017870133234));
#20380=CARTESIAN_POINT('Ctrl Pts',(1.91027492854846,-2.62599231814139,2.4181735923324));
#20381=CARTESIAN_POINT('Ctrl Pts',(3.24311081177889,0.16497767954115,2.57616848333245));
#20382=CARTESIAN_POINT('Ctrl Pts',(1.63393412158284,2.80628649337991,2.7341633743325));
#20383=CARTESIAN_POINT('Ctrl Pts',(-1.45747813791209,2.90185159477728,2.89215826533256));
#20384=CARTESIAN_POINT('Ctrl Pts',(-3.22672816390422,0.364980032144142,
3.05015315633261));
#20385=CARTESIAN_POINT('Ctrl Pts',(-2.06882739509817,-2.50298585443527,
3.20814804733266));
#20386=CARTESIAN_POINT('Ctrl Pts',(0.965825724890286,-3.10034929240489,
3.36614293833272));
#20387=CARTESIAN_POINT('Ctrl Pts',(3.1243227658749,-0.885207486870811,3.52413782933277));
#20388=CARTESIAN_POINT('Ctrl Pts',(2.44856686017853,2.13295695269892,3.68213272033283));
#20389=CARTESIAN_POINT('Ctrl Pts',(-0.448424924558006,3.21619342238995,
3.84012761133287));
#20390=CARTESIAN_POINT('Ctrl Pts',(-2.9386246603379,1.3818357877601,3.99812250233293));
#20391=CARTESIAN_POINT('Ctrl Pts',(-2.76302888818086,-1.70606459460131,
4.15611739333298));
#20392=CARTESIAN_POINT('Ctrl Pts',(-0.0809306368842651,-3.24629562294995,
4.31411228433304));
#20393=CARTESIAN_POINT('Ctrl Pts',(2.67458445172116,-1.84162511099097,4.47210717533309));
#20394=CARTESIAN_POINT('Ctrl Pts',(3.00383009796752,1.23368949956199,4.63010206633314));
#20395=CARTESIAN_POINT('Ctrl Pts',(0.608128632616327,3.18985338302612,4.7880969573332));
#20396=CARTESIAN_POINT('Ctrl Pts',(-2.33924130497153,2.25231772980782,4.94609184833325));
#20397=CARTESIAN_POINT('Ctrl Pts',(-3.16455086313379,-0.728424926493586,
5.10408673933331));
#20398=CARTESIAN_POINT('Ctrl Pts',(-1.11911425628133,-3.04837142099104,
5.26208163033336));
#20399=CARTESIAN_POINT('Ctrl Pts',(1.94153528232519,-2.60296480698359,5.42007652133342));
#20400=CARTESIAN_POINT('Ctrl Pts',(3.24090645725565,0.20374094882929,5.57807141233347));
#20401=CARTESIAN_POINT('Ctrl Pts',(1.60026491450814,2.82562156742707,5.73606630333352));
#20402=CARTESIAN_POINT('Ctrl Pts',(-1.49206900577688,2.8842182859333,5.89406119433358));
#20403=CARTESIAN_POINT('Ctrl Pts',(-3.23086128254485,0.326374649544494,
6.05205608533362));
#20404=CARTESIAN_POINT('Ctrl Pts',(-2.03875339757824,-2.52754220989012,
6.21005097633369));
#20405=CARTESIAN_POINT('Ctrl Pts',(1.00282499699587,-3.08858010488847,6.36804586733373));
#20406=CARTESIAN_POINT('Ctrl Pts',(3.1346831377893,-0.847789280760374,6.52604075833379));
#20407=CARTESIAN_POINT('Ctrl Pts',(2.42288984570632,2.16207997874408,6.68403564933384));
#20408=CARTESIAN_POINT('Ctrl Pts',(-0.486846229934527,3.21060209108997,
6.8420305403339));
#20409=CARTESIAN_POINT('Ctrl Pts',(-2.95493607899053,1.34660231991219,7.00002543133394));
#20410=CARTESIAN_POINT('Ctrl Pts',(-2.74243339421689,-1.73897789439567,
7.15802032233401));
#20411=CARTESIAN_POINT('Ctrl Pts',(-0.042111587625147,-3.24703120605584,
7.31601521333405));
#20412=CARTESIAN_POINT('Ctrl Pts',(2.69641206305327,-1.80951568800428,7.47401010433411));
#20413=CARTESIAN_POINT('Ctrl Pts',(2.98886518931682,1.26951562377266,7.63200499533417));
#20414=CARTESIAN_POINT('Ctrl Pts',(0.56994673361268,3.19689626978371,7.78999988633422));
#20415=CARTESIAN_POINT('Ctrl Pts',(-2.36600319687202,2.2241883713625,7.94799477733426));
#20416=CARTESIAN_POINT('Ctrl Pts',(-3.15561549601314,-0.766208770658805,
8.10598966833433));
#20417=CARTESIAN_POINT('Ctrl Pts',(-1.0825874157591,-3.06153385187112,8.26398455933438));
#20418=CARTESIAN_POINT('Ctrl Pts',(1.97251799758337,-2.57956542621475,8.42197945033443));
#20419=CARTESIAN_POINT('Ctrl Pts',(3.23823884360454,0.242475216637791,8.57997434133449));
#20420=CARTESIAN_POINT('Ctrl Pts',(1.566366917775,2.84455263931128,8.73796923233454));
#20421=CARTESIAN_POINT('Ctrl Pts',(-1.52644656238412,2.86617269736115,8.89596412333459));
#20422=CARTESIAN_POINT('Ctrl Pts',(-3.23453253946489,0.287722592188601,
9.05395901433465));
#20423=CARTESIAN_POINT('Ctrl Pts',(-2.0083879464276,-2.55173723089919,9.21195390533469));
#20424=CARTESIAN_POINT('Ctrl Pts',(1.0396809083576,-3.07636939389751,9.36994879633477));
#20425=CARTESIAN_POINT('Ctrl Pts',(3.14459539160713,-0.810249876270418,
9.5279436873348));
#20426=CARTESIAN_POINT('Ctrl Pts',(2.39686646622593,2.19089392303558,9.68593857833487));
#20427=CARTESIAN_POINT('Ctrl Pts',(-0.525197937892946,3.20455178846357,
9.8439334693349));
#20428=CARTESIAN_POINT('Ctrl Pts',(-2.97082507451666,1.31117634799362,10.001928360335));
#20429=CARTESIAN_POINT('Ctrl Pts',(-2.72144585527141,-1.77164259819448,
10.159923251335));
#20430=CARTESIAN_POINT('Ctrl Pts',(-0.00328651833606387,-3.24730260950622,
10.3179181423351));
#20431=CARTESIAN_POINT('Ctrl Pts',(2.71785420847995,-1.77714758542301,10.4759130333351));
#20432=CARTESIAN_POINT('Ctrl Pts',(2.97347300705285,1.30516026419214,10.6339079243352));
#20433=CARTESIAN_POINT('Ctrl Pts',(0.531683357813799,3.20348214384215,10.7919028153352));
#20434=CARTESIAN_POINT('Ctrl Pts',(-2.39242685650282,2.19574105378912,10.9498977063353));
#20435=CARTESIAN_POINT('Ctrl Pts',(-3.14622901745573,-0.803883081364814,
11.1078925973353));
#20436=CARTESIAN_POINT('Ctrl Pts',(-1.0459058138638,-3.07425862076485,11.2658874883354));
#20437=CARTESIAN_POINT('Ctrl Pts',(2.00321873137213,-2.55579728340303,11.4238823793354));
#20438=CARTESIAN_POINT('Ctrl Pts',(3.23510830694092,0.281174821482934,11.5818772703355));
#20439=CARTESIAN_POINT('Ctrl Pts',(1.5322450011872,2.86307706760007,11.7398721613356));
#20440=CARTESIAN_POINT('Ctrl Pts',(-1.56060590625239,2.84771737511982,11.8978670523356));
#20441=CARTESIAN_POINT('Ctrl Pts',(-3.23774140219028,0.2490294026297,12.0558619433357));
#20442=CARTESIAN_POINT('Ctrl Pts',(-1.97773538819436,-2.57556746649356,
12.2138568343357));
#20443=CARTESIAN_POINT('Ctrl Pts',(1.07638819633982,-3.06371890299285,12.3718517253358));
#20444=CARTESIAN_POINT('Ctrl Pts',(3.15405810111051,-0.772594636941618,
12.5298466163358));
#20445=CARTESIAN_POINT('Ctrl Pts',(2.37050045822502,2.21939465736754,12.6878415073359));
#20446=CARTESIAN_POINT('Ctrl Pts',(-0.563474596353531,3.19804339868417,
12.8458363983359));
#20447=CARTESIAN_POINT('Ctrl Pts',(-2.98628931759431,1.2755628985751,13.003831289336));
#20448=CARTESIAN_POINT('Ctrl Pts',(-2.70006938207651,-1.80405396377073,
13.161826180336));
#20449=CARTESIAN_POINT('Ctrl Pts',(0.0355392316804697,-3.24710993355476,
13.3198210713361));
#20450=CARTESIAN_POINT('Ctrl Pts',(2.73890741976546,-1.74452516462138,13.4778159623361));
#20451=CARTESIAN_POINT('Ctrl Pts',(2.95765652145599,1.3406178173039,13.6358108533362));
#20452=CARTESIAN_POINT('Ctrl Pts',(0.493342504231463,3.20961103420941,13.7938057443362));
#20453=CARTESIAN_POINT('Ctrl Pts',(-2.41850569611158,2.16697798953759,13.9518006353363));
#20454=CARTESIAN_POINT('Ctrl Pts',(-3.13639813875855,-0.841438930159867,
14.1097955263364));
#20455=CARTESIAN_POINT('Ctrl Pts',(-1.00906443556115,-3.08655067730993,
14.2677904173364));
#20456=CARTESIAN_POINT('Ctrl Pts',(2.03361349431715,-2.53165084404301,14.4257853083365));
#20457=CARTESIAN_POINT('Ctrl Pts',(3.23155274358889,0.319809522622996,14.5837801993365));
#20458=CARTESIAN_POINT('Ctrl Pts',(1.49783249263057,2.88123941244982,14.7417750903366));
#20459=CARTESIAN_POINT('Ctrl Pts',(-1.59440544683904,2.8287647573801,14.8997699813366));
#20460=CARTESIAN_POINT('Ctrl Pts',(-3.24074864036727,0.210472984148126,
15.0577648723367));
#20461=CARTESIAN_POINT('Ctrl Pts',(-1.94630068488002,-2.59935916099094,
15.2157597633367));
#20462=CARTESIAN_POINT('Ctrl Pts',(1.1119846044715,-3.04999779215944,15.3737546543368));
#20463=CARTESIAN_POINT('Ctrl Pts',(3.16492337134089,-0.73606266996359,15.5317495453368));
#20464=CARTESIAN_POINT('Ctrl Pts',(2.34003295606631,2.25015547162033,15.6897444363369));
#20465=CARTESIAN_POINT('Ctrl Pts',(0.384968583225142,2.87299014350137,15.7950743636703));
#20466=CARTESIAN_POINT('Ctrl Pts',(-0.50988368525085,2.70426773226927,15.847739327337));
#20467=CARTESIAN_POINT('Ctrl Pts',(-1.28892185405322,2.64462557919718,-2.77555756156289E-16));
#20468=CARTESIAN_POINT('Ctrl Pts',(-2.16403831185614,2.21811653527943,0.0526649636666843));
#20469=CARTESIAN_POINT('Ctrl Pts',(-3.44311483358514,0.436018596449888,
0.157994891000053));
#20470=CARTESIAN_POINT('Ctrl Pts',(-2.24436477004298,-2.65148082752247,
0.315989782000107));
#20471=CARTESIAN_POINT('Ctrl Pts',(0.99325262796079,-3.32545480540779,0.47398467300016));
#20472=CARTESIAN_POINT('Ctrl Pts',(3.32835797506399,-0.986820490209951,
0.631979564000214));
#20473=CARTESIAN_POINT('Ctrl Pts',(2.64488728032712,2.24914078759987,0.789974455000268));
#20474=CARTESIAN_POINT('Ctrl Pts',(-0.438314957393884,3.44366717194826,
0.947969346000321));
#20475=CARTESIAN_POINT('Ctrl Pts',(-3.12368605475517,1.51482555164407,1.10596423700038));
#20476=CARTESIAN_POINT('Ctrl Pts',(-2.97549193622185,-1.78850534874892,
1.26395912800043));
#20477=CARTESIAN_POINT('Ctrl Pts',(-0.128000241792142,-3.46922110496824,
1.42195401900048));
#20478=CARTESIAN_POINT('Ctrl Pts',(2.83557766746782,-2.00289002972017,1.57994891000054));
#20479=CARTESIAN_POINT('Ctrl Pts',(3.22685571589167,1.28042139796218,1.73794380100059));
#20480=CARTESIAN_POINT('Ctrl Pts',(0.690859017896064,3.40216610167957,1.89593869200064));
#20481=CARTESIAN_POINT('Ctrl Pts',(-2.47185131912304,2.43762212093852,2.0539335830007));
#20482=CARTESIAN_POINT('Ctrl Pts',(-3.39220536703243,-0.738235384598252,
2.21192847400075));
#20483=CARTESIAN_POINT('Ctrl Pts',(-1.23529356600166,-3.24439382779317,
2.3699233650008));
#20484=CARTESIAN_POINT('Ctrl Pts',(2.0422234829505,-2.80737767009854,2.52791825600086));
#20485=CARTESIAN_POINT('Ctrl Pts',(3.46712243282082,0.176373194395425,2.68591314700091));
#20486=CARTESIAN_POINT('Ctrl Pts',(1.74679496800295,3.00012531757514,2.84390803800096));
#20487=CARTESIAN_POINT('Ctrl Pts',(-1.55815062776997,3.10229139393809,3.00190292900102));
#20488=CARTESIAN_POINT('Ctrl Pts',(-3.44960818515806,0.390190323556838,
3.15989782000107));
#20489=CARTESIAN_POINT('Ctrl Pts',(-2.21172765516599,-2.67587477227939,
3.31789271100113));
#20490=CARTESIAN_POINT('Ctrl Pts',(1.03253827306805,-3.31449993698521,3.47588760200118));
#20491=CARTESIAN_POINT('Ctrl Pts',(3.34012933187316,-0.946351485827688,
3.63388249300123));
#20492=CARTESIAN_POINT('Ctrl Pts',(2.61769689100758,2.28028683820616,3.79187738400129));
#20493=CARTESIAN_POINT('Ctrl Pts',(-0.479399010889233,3.43834577670275,
3.94987227500134));
#20494=CARTESIAN_POINT('Ctrl Pts',(-3.14160448804072,1.4772834282495,4.1078671660014));
#20495=CARTESIAN_POINT('Ctrl Pts',(-2.95387977677187,-1.82390771425382,
4.26586205700145));
#20496=CARTESIAN_POINT('Ctrl Pts',(-0.0865207644539496,-3.47052722867774,
4.4238569480015));
#20497=CARTESIAN_POINT('Ctrl Pts',(2.85932621153631,-1.96883181171989,4.58185183900155));
#20498=CARTESIAN_POINT('Ctrl Pts',(3.21131386544667,1.31890422107427,4.73984673000161));
#20499=CARTESIAN_POINT('Ctrl Pts',(0.65013394439898,3.41018634994864,4.89784162100166));
#20500=CARTESIAN_POINT('Ctrl Pts',(-2.50081988404187,2.40789223066154,5.05583651200171));
#20501=CARTESIAN_POINT('Ctrl Pts',(-3.38313610732142,-0.77873947263813,
5.21383140300178));
#20502=CARTESIAN_POINT('Ctrl Pts',(-1.19641491396169,-3.25893179440594,
5.37182629400181));
#20503=CARTESIAN_POINT('Ctrl Pts',(2.07564308534076,-2.78275957804407,5.52982118500188));
#20504=CARTESIAN_POINT('Ctrl Pts',(3.46476581676266,0.217813961707557,5.68781607600192));
#20505=CARTESIAN_POINT('Ctrl Pts',(1.71080012542156,3.02079592455092,5.84581096700199));
#20506=CARTESIAN_POINT('Ctrl Pts',(-1.59513079308199,3.08344009831299,6.00380585800203));
#20507=CARTESIAN_POINT('Ctrl Pts',(-3.45402679099304,0.348918348651528,
6.1618007490021));
#20508=CARTESIAN_POINT('Ctrl Pts',(-2.17957635430163,-2.7021273106005,6.31979564000214));
#20509=CARTESIAN_POINT('Ctrl Pts',(1.07209319849625,-3.30191781555228,6.4777905310022));
#20510=CARTESIAN_POINT('Ctrl Pts',(3.35120532648497,-0.906348689336672,
6.63578542200224));
#20511=CARTESIAN_POINT('Ctrl Pts',(2.59024628631004,2.31142148107623,6.79378031300231));
#20512=CARTESIAN_POINT('Ctrl Pts',(-0.520474193792445,3.4323682349829,6.95177520400236));
#20513=CARTESIAN_POINT('Ctrl Pts',(-3.15904258646038,1.43961627660056,7.10977009500241));
#20514=CARTESIAN_POINT('Ctrl Pts',(-2.93186168880579,-1.85909443671817,
7.26776498600247));
#20515=CARTESIAN_POINT('Ctrl Pts',(-0.0450203642769841,-3.47131362076721,
7.42575987700253));
#20516=CARTESIAN_POINT('Ctrl Pts',(2.8826615230001,-1.93450449230244,7.58375476800256));
#20517=CARTESIAN_POINT('Ctrl Pts',(3.19531528460895,1.35720496568057,7.74174965900264));
#20518=CARTESIAN_POINT('Ctrl Pts',(0.609314704401862,3.41771571051825,7.89974455000267));
#20519=CARTESIAN_POINT('Ctrl Pts',(-2.52943030198254,2.37781989106326,8.05773944100274));
#20520=CARTESIAN_POINT('Ctrl Pts',(-3.37358354695964,-0.819133162926983,
8.21573433200278));
#20521=CARTESIAN_POINT('Ctrl Pts',(-1.15736505241679,-3.27300339479932,
8.37372922300284));
#20522=CARTESIAN_POINT('Ctrl Pts',(2.10876587186757,-2.75774393020277,8.53172411400289));
#20523=CARTESIAN_POINT('Ctrl Pts',(3.46191394284634,0.259223724318805,8.68971900500295));
#20524=CARTESIAN_POINT('Ctrl Pts',(1.67456068997757,3.04103462369395,8.847713896003));
#20525=CARTESIAN_POINT('Ctrl Pts',(-1.63188291307296,3.06414804553306,9.00570878700305));
#20526=CARTESIAN_POINT('Ctrl Pts',(-3.45795163290035,0.307596475021262,
9.16370367800311));
#20527=CARTESIAN_POINT('Ctrl Pts',(-2.14711346820945,-2.72799355599627,
9.32169856900316));
#20528=CARTESIAN_POINT('Ctrl Pts',(1.11149486081386,-3.28886367326282,9.47969346000322));
#20529=CARTESIAN_POINT('Ctrl Pts',(3.36180225010744,-0.866216322921951,
9.63768835100326));
#20530=CARTESIAN_POINT('Ctrl Pts',(2.56242539210976,2.34222569296695,9.79568324200333));
#20531=CARTESIAN_POINT('Ctrl Pts',(-0.561474971970195,3.42590001937795,
9.95367813300337));
#20532=CARTESIAN_POINT('Ctrl Pts',(-3.17602908369125,1.40174332403378,10.1116730240034));
#20533=CARTESIAN_POINT('Ctrl Pts',(-2.90942447610763,-1.8940153918983,10.2696679150035));
#20534=CARTESIAN_POINT('Ctrl Pts',(-0.0035135282481055,-3.47160377088719,
10.4276628060035));
#20535=CARTESIAN_POINT('Ctrl Pts',(2.90558474324488,-1.89990062549661,10.5856576970036));
#20536=CARTESIAN_POINT('Ctrl Pts',(3.17885991705762,1.39531169085301,10.7436525880036));
#20537=CARTESIAN_POINT('Ctrl Pts',(0.568408359757113,3.4247564911184,10.9016474790037));
#20538=CARTESIAN_POINT('Ctrl Pts',(-2.55767912491219,2.34740762992373,11.0596423700038));
#20539=CARTESIAN_POINT('Ctrl Pts',(-3.36354871550911,-0.859409753944302,
11.2176372610038));
#20540=CARTESIAN_POINT('Ctrl Pts',(-1.11814973965565,-3.2866071025492,11.3756321520039));
#20541=CARTESIAN_POINT('Ctrl Pts',(2.14158719959911,-2.73233404879208,11.5336270430039));
#20542=CARTESIAN_POINT('Ctrl Pts',(3.45856717040372,0.300596429689395,11.691621934004));
#20543=CARTESIAN_POINT('Ctrl Pts',(1.63808186784707,3.0608385911199,11.849616825004));
#20544=CARTESIAN_POINT('Ctrl Pts',(-1.66840174770112,3.04441795752144,12.0076117160041));
#20545=CARTESIAN_POINT('Ctrl Pts',(-3.46138214162631,0.266230628060431,
12.1656066070041));
#20546=CARTESIAN_POINT('Ctrl Pts',(-2.11434364366697,-2.75346981912873,
12.3236014980042));
#20547=CARTESIAN_POINT('Ctrl Pts',(1.15073763387882,-3.27533937411076,12.4815963890042));
#20548=CARTESIAN_POINT('Ctrl Pts',(3.37191857800943,-0.825960120600417,
12.6395912800043));
#20549=CARTESIAN_POINT('Ctrl Pts',(2.53423820298509,2.37269506052457,12.7975861710043));
#20550=CARTESIAN_POINT('Ctrl Pts',(-0.602395516750883,3.41894207513388,
12.9555810620044));
#20551=CARTESIAN_POINT('Ctrl Pts',(-3.19256148951789,1.3636699443205,13.1135759530045));
#20552=CARTESIAN_POINT('Ctrl Pts',(-2.8865714642773,-1.928665510007,13.2715708440045));
#20553=CARTESIAN_POINT('Ctrl Pts',(0.0379940355281645,-3.4713977862162,
13.4295657350046));
#20554=CARTESIAN_POINT('Ctrl Pts',(2.92809216447323,-1.8650248739301,13.5875606260046));
#20555=CARTESIAN_POINT('Ctrl Pts',(3.16195093823948,1.43321840602296,13.7455555170047));
#20556=CARTESIAN_POINT('Ctrl Pts',(0.527419185700519,3.43130872276077,13.9035504080047));
#20557=CARTESIAN_POINT('Ctrl Pts',(-2.58555931004217,2.31665781251357,14.0615452990048));
#20558=CARTESIAN_POINT('Ctrl Pts',(-3.35303878783672,-0.89955970052277,
14.2195401900048));
#20559=CARTESIAN_POINT('Ctrl Pts',(-1.07876361424012,-3.29974820917995,
14.3775350810049));
#20560=CARTESIAN_POINT('Ctrl Pts',(2.1740814221413,-2.70651974072904,14.5355299720049));
#20561=CARTESIAN_POINT('Ctrl Pts',(3.45476601337439,0.341899748256715,14.693524863005));
#20562=CARTESIAN_POINT('Ctrl Pts',(1.60129238166824,3.08025546489199,14.851519754005));
#20563=CARTESIAN_POINT('Ctrl Pts',(-1.70453592633028,3.02415622428451,15.0095146450051));
#20564=CARTESIAN_POINT('Ctrl Pts',(-3.46459709897726,0.225010999375169,
15.1675095360052));
#20565=CARTESIAN_POINT('Ctrl Pts',(-2.08073764888123,-2.77890487901232,
15.3255044270052));
#20566=CARTESIAN_POINT('Ctrl Pts',(1.18879279521126,-3.26067050402438,15.4834993180053));
#20567=CARTESIAN_POINT('Ctrl Pts',(3.38353434581409,-0.786904778499691,
15.6414942090053));
#20568=CARTESIAN_POINT('Ctrl Pts',(2.50166621690838,2.40558061866225,15.7994891000054));
#20569=CARTESIAN_POINT('Ctrl Pts',(0.411559545231536,3.07143639360967,15.9048190273387));
#20570=CARTESIAN_POINT('Ctrl Pts',(-0.545102916879006,2.891059807408,15.9574839910054));
#20571=CARTESIAN_POINT('Ctrl Pts',(-2.94111188951679,-0.00259486169482749,
14.1778238829104));
#20572=CARTESIAN_POINT('Ctrl Pts',(-2.94335307565858,-0.259762554464039,
14.1917293186085));
#20573=CARTESIAN_POINT('Ctrl Pts',(-2.91238767988341,-0.516399492336486,
14.2056347543067));
#20574=CARTESIAN_POINT('Ctrl Pts',(-2.84607967927153,-0.763554866459577,
14.2195401900048));
#20575=CARTESIAN_POINT('Ctrl Pts',(-2.59494706330453,-1.69962253674182,
14.2722051536715));
#20576=CARTESIAN_POINT('Ctrl Pts',(-1.83685533877235,-2.49968537296086,
14.3248701173382));
#20577=CARTESIAN_POINT('Ctrl Pts',(-0.915668637109368,-2.80084537966192,
14.3775350810049));
#20578=CARTESIAN_POINT('Ctrl Pts',(0.00551806455364026,-3.10200538636298,
14.4302000446716));
#20579=CARTESIAN_POINT('Ctrl Pts',(1.0897997433475,-2.90426256354601,14.4828650083382));
#20580=CARTESIAN_POINT('Ctrl Pts',(1.84538801461659,-2.29732123730656,14.5355299720049));
#20581=CARTESIAN_POINT('Ctrl Pts',(2.60097628588567,-1.6903799110671,14.5881949356716));
#20582=CARTESIAN_POINT('Ctrl Pts',(3.02787114963004,-0.674240081405173,
14.6408598993383));
#20583=CARTESIAN_POINT('Ctrl Pts',(2.93240630955118,0.29022245286501,14.693524863005));
#20584=CARTESIAN_POINT('Ctrl Pts',(2.83694146947232,1.25468498713517,14.7461898266717));
#20585=CARTESIAN_POINT('Ctrl Pts',(2.21911692557029,2.16747022601356,14.7988547903384));
#20586=CARTESIAN_POINT('Ctrl Pts',(1.35923326895286,2.61451297201819,14.851519754005));
#20587=CARTESIAN_POINT('Ctrl Pts',(0.499349612335403,3.06155571802283,14.9041847176717));
#20588=CARTESIAN_POINT('Ctrl Pts',(-0.602593156997484,3.04285597115367,
14.9568496813384));
#20589=CARTESIAN_POINT('Ctrl Pts',(-1.4469080704384,2.56698189356751,15.0095146450051));
#20590=CARTESIAN_POINT('Ctrl Pts',(-1.70601080500511,2.42094600950443,15.0256764300034));
#20591=CARTESIAN_POINT('Ctrl Pts',(-1.94085146734146,2.2318557880317,15.0418382150017));
#20592=CARTESIAN_POINT('Ctrl Pts',(-2.14373220034761,2.01193738948431,15.058));
#20593=CARTESIAN_POINT('Ctrl Pts',(-1.37994859234592,-1.93347131995891,
-1.83880688453542E-16));
#20594=CARTESIAN_POINT('Ctrl Pts',(-1.43831895271373,-1.90176082500493,
-1.96503831907269E-16));
#20595=CARTESIAN_POINT('Ctrl Pts',(-1.49514575458196,-1.86752259046863,
-3.60259795903682E-17));
#20596=CARTESIAN_POINT('Ctrl Pts',(-1.55024291463987,-1.83079524515745,
-1.11022302462516E-16));
#20597=CARTESIAN_POINT('Ctrl Pts',(-1.61820139003649,-1.78549464545158,
-1.89647209120044E-16));
#20598=CARTESIAN_POINT('Ctrl Pts',(-1.68352982136479,-1.73640902813589,
4.37133882625492E-17));
#20599=CARTESIAN_POINT('Ctrl Pts',(-1.74614398662112,-1.68389593204229,
2.08166817117217E-17));
#20600=CARTESIAN_POINT('Ctrl Pts',(-1.78291149355231,-1.65305984859862,
7.3715640875763E-18));
#20601=CARTESIAN_POINT('Ctrl Pts',(-1.81874277362574,-1.62104095184393,
-1.13501056944751E-16));
#20602=CARTESIAN_POINT('Ctrl Pts',(-1.85361742493061,-1.58790418430478,
-1.38777878078145E-16));
#20603=CARTESIAN_POINT('Ctrl Pts',(-1.86599100473682,-1.57614720832583,
-1.47746133009421E-16));
#20604=CARTESIAN_POINT('Ctrl Pts',(-1.87824533378606,-1.56424827137885,
6.18933070998169E-17));
#20605=CARTESIAN_POINT('Ctrl Pts',(-1.89037564784625,-1.55221386701801,
6.93889390390723E-18));
#20606=CARTESIAN_POINT('Ctrl Pts',(-1.9520612058093,-1.49101603289205,-2.72517484859507E-16));
#20607=CARTESIAN_POINT('Ctrl Pts',(-2.01038866542646,-1.42647262579372,
-5.93465220813464E-16));
#20608=CARTESIAN_POINT('Ctrl Pts',(-2.06526482907838,-1.35900295762991,
-3.95516952522712E-16));
#20609=CARTESIAN_POINT('Ctrl Pts',(-2.11328147227381,-1.29996699798658,
-2.22312217768304E-16));
#20610=CARTESIAN_POINT('Ctrl Pts',(-2.15865566139155,-1.2386893890933,-3.33360010116584E-16));
#20611=CARTESIAN_POINT('Ctrl Pts',(-2.20130818996771,-1.17541961668097,
-3.46944695195361E-16));
#20612=CARTESIAN_POINT('Ctrl Pts',(-2.22006840714514,-1.1475911452903,-3.52919760469855E-16));
#20613=CARTESIAN_POINT('Ctrl Pts',(-2.23830186692143,-1.11937693173939,
-3.24730293914024E-16));
#20614=CARTESIAN_POINT('Ctrl Pts',(-2.25600064404541,-1.09079672684346,
-3.05311331771918E-16));
#20615=CARTESIAN_POINT('Ctrl Pts',(-2.26668277274188,-1.07354709288677,
-2.93590982320615E-16));
#20616=CARTESIAN_POINT('Ctrl Pts',(-2.27717011522814,-1.05616412126237,
7.72460434588031E-17));
#20617=CARTESIAN_POINT('Ctrl Pts',(-2.28746078556243,-1.03865201740679,
1.38777878078145E-16));
#20618=CARTESIAN_POINT('Ctrl Pts',(-2.2952947631346,-1.02532057986291,1.85620211640871E-16));
#20619=CARTESIAN_POINT('Ctrl Pts',(-2.30301001735291,-1.01192234024488,
-2.74638834286083E-16));
#20620=CARTESIAN_POINT('Ctrl Pts',(-2.31060459934883,-0.99846213025753,
-2.77555756156289E-16));
#20621=CARTESIAN_POINT('Ctrl Pts',(-2.35418081118604,-0.921230103254969,
-2.94292477860916E-16));
#20622=CARTESIAN_POINT('Ctrl Pts',(-2.39380271969424,-0.841933889485626,
-3.78845217127159E-17));
#20623=CARTESIAN_POINT('Ctrl Pts',(-2.42937389319446,-0.760969916140703,
-6.93889390390723E-17));
#20624=CARTESIAN_POINT('Ctrl Pts',(-2.46720610926394,-0.674859556767564,
-1.02895900045749E-16));
#20625=CARTESIAN_POINT('Ctrl Pts',(-2.5004573035107,-0.586862180324133,
-9.42383278312778E-17));
#20626=CARTESIAN_POINT('Ctrl Pts',(-2.52897137574918,-0.497406668002497,
0.));
#20627=CARTESIAN_POINT('Ctrl Pts',(-2.55035692992803,-0.430315033761271,
7.06787458734584E-17));
#20628=CARTESIAN_POINT('Ctrl Pts',(-2.56907707912655,-0.362402071614612,
2.24154037051898E-16));
#20629=CARTESIAN_POINT('Ctrl Pts',(-2.58504714386116,-0.293835873442853,
2.77555756156289E-16));
#20630=CARTESIAN_POINT('Ctrl Pts',(-2.59702469241211,-0.242411224814034,
3.17607045484582E-16));
#20631=CARTESIAN_POINT('Ctrl Pts',(-2.60745499960513,-0.1906188874626,1.72939271916983E-16));
#20632=CARTESIAN_POINT('Ctrl Pts',(-2.61629539664834,-0.138527206391925,
1.38777878078145E-16));
#20633=CARTESIAN_POINT('Ctrl Pts',(-2.61869711284596,-0.124375191094725,
1.29497076264031E-16));
#20634=CARTESIAN_POINT('Ctrl Pts',(-2.62098183196127,-0.110198515695441,
1.70346493820844E-17));
#20635=CARTESIAN_POINT('Ctrl Pts',(-2.62314735205575,-0.0960068887486099,
2.77555756156289E-17));
#20636=CARTESIAN_POINT('Ctrl Pts',(-2.63712677206149,-0.00439346333649258,
9.69640447732094E-17));
#20637=CARTESIAN_POINT('Ctrl Pts',(-2.64610759043344,0.0876011416361361,
-2.12521409618605E-16));
#20638=CARTESIAN_POINT('Ctrl Pts',(-2.64996359474771,0.179577964648124,
-5.55111512312578E-17));
#20639=CARTESIAN_POINT('Ctrl Pts',(-2.65210628483955,0.230687302523444,
3.17357233945851E-17));
#20640=CARTESIAN_POINT('Ctrl Pts',(-2.65266584064783,0.281791760322423,
2.25858622101648E-16));
#20641=CARTESIAN_POINT('Ctrl Pts',(-2.65161463128253,0.332826444242184,
1.94289029309402E-16));
#20642=CARTESIAN_POINT('Ctrl Pts',(-2.64978728963931,0.421541220055518,
1.40408657934648E-16));
#20643=CARTESIAN_POINT('Ctrl Pts',(-2.6430958113368,0.510044886368098,1.72520161624302E-16));
#20644=CARTESIAN_POINT('Ctrl Pts',(-2.63178393076928,0.598076371345786,
1.66533453693773E-16));
#20645=CARTESIAN_POINT('Ctrl Pts',(-2.62024798910265,0.687851547937211,
1.60428163503557E-16));
#20646=CARTESIAN_POINT('Ctrl Pts',(-2.60390669120625,0.777136386959749,
-1.34425914858345E-16));
#20647=CARTESIAN_POINT('Ctrl Pts',(-2.58296460883121,0.865656938831555,
-1.11022302462516E-16));
#20648=CARTESIAN_POINT('Ctrl Pts',(-2.57869408333521,0.883708117645516,
-1.06249819877211E-16));
#20649=CARTESIAN_POINT('Ctrl Pts',(-2.57423206760738,0.901727502426255,
-4.70036822748448E-17));
#20650=CARTESIAN_POINT('Ctrl Pts',(-2.56958003501042,0.919712740461561,
-5.55111512312578E-17));
#20651=CARTESIAN_POINT('Ctrl Pts',(-2.56604635272843,0.933374320783267,
-6.19734215806574E-17));
#20652=CARTESIAN_POINT('Ctrl Pts',(-2.56240532303519,0.947007284078113,
8.26362614469453E-17));
#20653=CARTESIAN_POINT('Ctrl Pts',(-2.5586586911495,0.960608258314244,8.32667268468867E-17));
#20654=CARTESIAN_POINT('Ctrl Pts',(-2.53407091484386,1.04986648337083,8.74042409382574E-17));
#20655=CARTESIAN_POINT('Ctrl Pts',(-2.504930952964,1.13777933274063,7.81122475311754E-16));
#20656=CARTESIAN_POINT('Ctrl Pts',(-2.47152838793823,1.2240648243653,6.38378239159465E-16));
#20657=CARTESIAN_POINT('Ctrl Pts',(-2.43748524526305,1.31200505589874,4.92896525595146E-16));
#20658=CARTESIAN_POINT('Ctrl Pts',(-2.39901427145562,1.39825569878996,-4.49689980744232E-17));
#20659=CARTESIAN_POINT('Ctrl Pts',(-2.35636659634517,1.48252101187545,-5.55111512312578E-17));
#20660=CARTESIAN_POINT('Ctrl Pts',(-2.31336109209446,1.56749334086406,-6.61417567970626E-17));
#20661=CARTESIAN_POINT('Ctrl Pts',(-2.26610821171127,1.65044775809861,-5.44480906746773E-17));
#20662=CARTESIAN_POINT('Ctrl Pts',(-2.21481327415801,1.731071203515,-5.55111512312578E-17));
#20663=CARTESIAN_POINT('Ctrl Pts',(-2.18401751630642,1.77947481253834,-5.61493770883036E-17));
#20664=CARTESIAN_POINT('Ctrl Pts',(-2.15176385823466,1.82703799978858,3.67516605336294E-16));
#20665=CARTESIAN_POINT('Ctrl Pts',(-2.11808850376184,1.87368930169054,3.88578058618805E-16));
#20666=CARTESIAN_POINT('Ctrl Pts',(-2.1089145366433,1.88639822536441,3.94315699184355E-16));
#20667=CARTESIAN_POINT('Ctrl Pts',(-2.09963412322397,1.89904053530927,1.84615714870052E-16));
#20668=CARTESIAN_POINT('Ctrl Pts',(-2.09025911328956,1.91160012317952,1.66533453693773E-16));
#20669=CARTESIAN_POINT('Ctrl Pts',(-2.03145402967869,1.99038058527982,5.31118266465956E-17));
#20670=CARTESIAN_POINT('Ctrl Pts',(-1.96883756375661,2.06603912302101,4.62847422951145E-16));
#20671=CARTESIAN_POINT('Ctrl Pts',(-1.90268196527442,2.13826743811961,3.33066907387547E-16));
#20672=CARTESIAN_POINT('Ctrl Pts',(-1.83635976195865,2.21067765145044,2.0295955537029E-16));
#20673=CARTESIAN_POINT('Ctrl Pts',(-1.76648017672323,2.2796412428746,3.28001727774597E-18));
#20674=CARTESIAN_POINT('Ctrl Pts',(-1.6932675195623,2.34483179093341,0.));
#20675=CARTESIAN_POINT('Ctrl Pts',(-1.62146081066126,2.40877044429043,-3.21702906282713E-18));
#20676=CARTESIAN_POINT('Ctrl Pts',(-1.54644728359632,2.46908034426641,-8.3280583097932E-18));
#20677=CARTESIAN_POINT('Ctrl Pts',(-1.46839770082455,2.52542611967769,-5.55111512312578E-17));
#20678=CARTESIAN_POINT('Ctrl Pts',(-1.41023968234018,2.56741172077267,-9.06692532072844E-17));
#20679=CARTESIAN_POINT('Ctrl Pts',(-1.35039506896231,2.60719581243537,-1.11866688105539E-17));
#20680=CARTESIAN_POINT('Ctrl Pts',(-1.28892185405323,2.64462557919718,0.));
#20681=CARTESIAN_POINT('Origin',(0.,0.,0.));
#20682=CARTESIAN_POINT('Origin',(-1.44337567297407,-2.5,-6.));
#20683=CARTESIAN_POINT('',(-1.44337567297407,-2.5,-6.));
#20684=CARTESIAN_POINT('',(1.44337567297406,-2.5,-6.));
#20685=CARTESIAN_POINT('',(-0.721687836487033,-2.5,-6.));
#20686=CARTESIAN_POINT('',(-1.44337567297407,-2.5,-3.));
#20687=CARTESIAN_POINT('',(-1.44337567297407,-2.5,-6.));
#20688=CARTESIAN_POINT('',(1.44337567297406,-2.5,-3.));
#20689=CARTESIAN_POINT('',(-1.44337567297407,-2.5,-3.));
#20690=CARTESIAN_POINT('',(1.44337567297406,-2.5,-6.));
#20691=CARTESIAN_POINT('Origin',(-2.88675134594813,3.53525079574969E-16,
-6.));
#20692=CARTESIAN_POINT('',(-2.88675134594813,3.53525079574969E-16,-6.));
#20693=CARTESIAN_POINT('',(-2.52590742770461,-0.625,-6.));
#20694=CARTESIAN_POINT('',(-2.88675134594813,5.55111512312578E-16,-3.));
#20695=CARTESIAN_POINT('',(-2.88675134594813,3.53525079574969E-16,-6.));
#20696=CARTESIAN_POINT('',(-2.88675134594813,3.53525079574969E-16,-3.));
#20697=CARTESIAN_POINT('Origin',(-1.44337567297406,2.5,-6.));
#20698=CARTESIAN_POINT('',(-1.44337567297406,2.5,-6.));
#20699=CARTESIAN_POINT('',(-1.80421959121758,1.875,-6.));
#20700=CARTESIAN_POINT('',(-1.44337567297406,2.5,-3.));
#20701=CARTESIAN_POINT('',(-1.44337567297406,2.5,-6.));
#20702=CARTESIAN_POINT('',(-1.44337567297406,2.5,-3.));
#20703=CARTESIAN_POINT('Origin',(1.44337567297406,2.5,-6.));
#20704=CARTESIAN_POINT('',(1.44337567297406,2.5,-6.));
#20705=CARTESIAN_POINT('',(0.721687836487033,2.5,-6.));
#20706=CARTESIAN_POINT('',(1.44337567297406,2.5,-3.));
#20707=CARTESIAN_POINT('',(1.44337567297406,2.5,-6.));
#20708=CARTESIAN_POINT('',(1.44337567297406,2.5,-3.));
#20709=CARTESIAN_POINT('Origin',(2.88675134594813,0.,-6.));
#20710=CARTESIAN_POINT('',(2.88675134594813,0.,-6.));
#20711=CARTESIAN_POINT('',(2.52590742770461,0.625,-6.));
#20712=CARTESIAN_POINT('',(2.88675134594813,0.,-3.));
#20713=CARTESIAN_POINT('',(2.88675134594813,0.,-6.));
#20714=CARTESIAN_POINT('',(2.88675134594813,0.,-3.));
#20715=CARTESIAN_POINT('Origin',(1.44337567297406,-2.5,-6.));
#20716=CARTESIAN_POINT('',(1.80421959121758,-1.875,-6.));
#20717=CARTESIAN_POINT('',(1.44337567297406,-2.5,-3.));
#20718=CARTESIAN_POINT('Origin',(0.,0.,-3.));
#20719=CARTESIAN_POINT('Origin',(0.,0.,0.));
#20720=CARTESIAN_POINT('',(-5.,-6.12323399573677E-16,0.));
#20721=CARTESIAN_POINT('Origin',(0.,0.,0.));
#20722=CARTESIAN_POINT('Origin',(0.,0.,-6.));
#20723=CARTESIAN_POINT('',(-5.,-6.12323399573677E-16,-6.));
#20724=CARTESIAN_POINT('',(-5.,-6.12323399573677E-16,-6.));
#20725=CARTESIAN_POINT('Origin',(0.,0.,-6.));
#20726=CARTESIAN_POINT('Origin',(0.,0.,-6.));
#20727=CARTESIAN_POINT('Origin',(0.,0.,16.));
#21865=UNCERTAINTY_MEASURE_WITH_UNIT(LENGTH_MEASURE(0.01),#21881,
'DISTANCE_ACCURACY_VALUE',
'Maximum model space distance between geometric entities at asserted c
onnectivities');
#21868=UNCERTAINTY_MEASURE_WITH_UNIT(LENGTH_MEASURE(0.01),#21881,
'DISTANCE_ACCURACY_VALUE',
'Maximum model space distance between geometric entities at asserted c
onnectivities');
#21877=(
GEOMETRIC_REPRESENTATION_CONTEXT(3)
GLOBAL_UNCERTAINTY_ASSIGNED_CONTEXT((#21865))
GLOBAL_UNIT_ASSIGNED_CONTEXT((#21881,#21883,#21884))
REPRESENTATION_CONTEXT('','3D')
);
#21880=(
GEOMETRIC_REPRESENTATION_CONTEXT(3)
GLOBAL_UNCERTAINTY_ASSIGNED_CONTEXT((#21868))
GLOBAL_UNIT_ASSIGNED_CONTEXT((#21881,#21883,#21884))
REPRESENTATION_CONTEXT('','3D')
);
#21881=(
LENGTH_UNIT()
NAMED_UNIT(*)
SI_UNIT(.MILLI.,.METRE.)
);
#21883=(
NAMED_UNIT(*)
PLANE_ANGLE_UNIT()
SI_UNIT($,.RADIAN.)
);
#21884=(
NAMED_UNIT(*)
SI_UNIT($,.STERADIAN.)
SOLID_ANGLE_UNIT()
);
#21893=SHAPE_DEFINITION_REPRESENTATION(#21904,#21932);
#21904=PRODUCT_DEFINITION_SHAPE('',$,#21944);
#21932=SHAPE_REPRESENTATION('',(#6864),#21877);
#21935=PRODUCT_DEFINITION_CONTEXT('part definition',#21970,'design');
#21944=PRODUCT_DEFINITION('Socket head cap screw M6x16',
'Socket head cap screw M6x16',#21955,#21935);
#21955=PRODUCT_DEFINITION_FORMATION('',$,#21980);
#21970=APPLICATION_CONTEXT(
'Core Data for Automotive Mechanical Design Process');
#21971=PRODUCT_CONTEXT('part definition',#21970,'mechanical');
#21980=PRODUCT('Socket head cap screw M6x16',
'Socket head cap screw M6x16',$,(#21971));
#21986=PRESENTATION_STYLE_ASSIGNMENT((#21992));
#21992=SURFACE_STYLE_USAGE(.BOTH.,#21998);
#21998=SURFACE_SIDE_STYLE('',(#22004));
#22004=SURFACE_STYLE_FILL_AREA(#22010);
#22010=FILL_AREA_STYLE('Dark gray',(#22016));
#22016=FILL_AREA_STYLE_COLOUR('Dark gray',#22022);
#22022=COLOUR_RGB('Dark gray',0.250980392156863,0.282352941176471,0.32156862745098);
ENDSEC;
END-ISO-10303-21;
